ISO-10303-21;
HEADER;
/* Generated by software containing ST-Developer
 * from STEP Tools, Inc. (www.steptools.com) 
 */

FILE_DESCRIPTION(
/* description */ (''),
/* implementation_level */ '2;1');

FILE_NAME(
/* name */ 'Bearing_03.step',
/* time_stamp */ '2026-10-05T21:54:13-07:00',
/* author */ (''),
/* organization */ (''),
/* preprocessor_version */ 'ST-DEVELOPER v20.2',
/* originating_system */ 'Autodesk Translation Framework v15.15.0.0',
/* authorisation */ '');

FILE_SCHEMA (('AUTOMOTIVE_DESIGN { 1 0 10303 214 3 1 1 }'));
ENDSEC;

DATA;
#10=MECHANICAL_DESIGN_GEOMETRIC_PRESENTATION_REPRESENTATION('',(#213,#214,#215,#216,#217,#218,#219,#220,#221,#222),#43781);
#71=SPHERICAL_SURFACE('',#14280,3.56616156686793);
#72=SPHERICAL_SURFACE('',#14282,3.56616156686793);
#73=SPHERICAL_SURFACE('',#14284,3.56616156686793);
#74=SPHERICAL_SURFACE('',#14286,3.56616156686793);
#75=SPHERICAL_SURFACE('',#14288,3.56616156686793);
#76=SPHERICAL_SURFACE('',#14290,3.56616156686793);
#77=SPHERICAL_SURFACE('',#14292,3.56616156686793);
#78=SPHERICAL_SURFACE('',#14346,3.56616156686792);
#79=SPHERICAL_SURFACE('',#14360,3.56616156686792);
#80=SPHERICAL_SURFACE('',#14374,3.56616156686792);
#81=SPHERICAL_SURFACE('',#14388,3.56616156686792);
#82=SPHERICAL_SURFACE('',#14402,3.56616156686792);
#83=SPHERICAL_SURFACE('',#14416,3.56616156686792);
#84=SPHERICAL_SURFACE('',#14426,3.56616156686792);
#107=CONICAL_SURFACE('',#14269,8.14999999999999,0.785398163397436);
#108=CONICAL_SURFACE('',#14272,7.5,0.785398163397437);
#109=CONICAL_SURFACE('',#14328,20.35,0.785398163397442);
#110=CONICAL_SURFACE('',#14331,21.,0.785398163397442);
#145=TOROIDAL_SURFACE('',#14254,14.25,3.56616156686793);
#146=TOROIDAL_SURFACE('',#14258,7.9875,0.4875);
#147=TOROIDAL_SURFACE('',#14264,7.9875,0.4875);
#148=TOROIDAL_SURFACE('',#14294,16.3271153846154,0.0585);
#149=TOROIDAL_SURFACE('',#14299,16.0931153846154,0.0585);
#150=TOROIDAL_SURFACE('',#14303,16.3271153846154,0.0585);
#151=TOROIDAL_SURFACE('',#14307,16.0931153846154,0.0585);
#152=TOROIDAL_SURFACE('',#14319,14.25,3.56616156686793);
#153=TOROIDAL_SURFACE('',#14342,2.5198520116158,1.69469015025);
#154=TOROIDAL_SURFACE('',#14356,2.5198520116158,1.69469015025);
#155=TOROIDAL_SURFACE('',#14370,2.5198520116158,1.69469015025);
#156=TOROIDAL_SURFACE('',#14384,2.5198520116158,1.69469015025);
#157=TOROIDAL_SURFACE('',#14398,2.5198520116158,1.69469015025);
#158=TOROIDAL_SURFACE('',#14412,2.5198520116158,1.69469015025);
#159=TOROIDAL_SURFACE('',#14436,2.5198520116158,1.69469015025);
#179=SHAPE_REPRESENTATION_RELATIONSHIP('SRR','None',#43817,#187);
#187=ADVANCED_BREP_SHAPE_REPRESENTATION('',(#257,#258,#259,#260,#261,#262,
#263,#264,#265,#266),#43777);
#213=STYLED_ITEM('',(#43863),#257);
#214=STYLED_ITEM('',(#43863),#258);
#215=STYLED_ITEM('',(#43863),#259);
#216=STYLED_ITEM('',(#43863),#260);
#217=STYLED_ITEM('',(#43863),#261);
#218=STYLED_ITEM('',(#43863),#262);
#219=STYLED_ITEM('',(#43863),#263);
#220=STYLED_ITEM('',(#43863),#264);
#221=STYLED_ITEM('',(#43863),#265);
#222=STYLED_ITEM('',(#43863),#266);
#257=MANIFOLD_SOLID_BREP('Body1',#13073);
#258=MANIFOLD_SOLID_BREP('Body2',#13074);
#259=MANIFOLD_SOLID_BREP('Body3',#13075);
#260=MANIFOLD_SOLID_BREP('Body4',#13076);
#261=MANIFOLD_SOLID_BREP('Body5',#13077);
#262=MANIFOLD_SOLID_BREP('Body6',#13078);
#263=MANIFOLD_SOLID_BREP('Body7',#13079);
#264=MANIFOLD_SOLID_BREP('Body8',#13080);
#265=MANIFOLD_SOLID_BREP('Body9',#13081);
#266=MANIFOLD_SOLID_BREP('Body10',#13082);
#383=FACE_BOUND('',#2646,.T.);
#384=FACE_BOUND('',#2648,.T.);
#385=FACE_BOUND('',#2671,.T.);
#386=FACE_BOUND('',#2673,.T.);
#387=FACE_BOUND('',#2675,.T.);
#388=FACE_BOUND('',#2677,.T.);
#389=FACE_BOUND('',#2679,.T.);
#390=FACE_BOUND('',#2681,.T.);
#391=FACE_BOUND('',#2683,.T.);
#392=FACE_BOUND('',#2684,.T.);
#393=FACE_BOUND('',#2686,.T.);
#394=FACE_BOUND('',#2687,.T.);
#395=FACE_BOUND('',#2689,.T.);
#396=FACE_BOUND('',#2690,.T.);
#397=FACE_BOUND('',#2692,.T.);
#398=FACE_BOUND('',#2693,.T.);
#399=FACE_BOUND('',#2695,.T.);
#400=FACE_BOUND('',#2696,.T.);
#401=FACE_BOUND('',#2698,.T.);
#402=FACE_BOUND('',#2699,.T.);
#403=FACE_BOUND('',#2701,.T.);
#404=FACE_BOUND('',#2702,.T.);
#405=FACE_BOUND('',#2704,.T.);
#406=FACE_BOUND('',#2705,.T.);
#407=FACE_BOUND('',#2707,.T.);
#408=FACE_BOUND('',#2708,.T.);
#409=FACE_BOUND('',#2710,.T.);
#410=FACE_BOUND('',#2711,.T.);
#411=FACE_BOUND('',#2713,.T.);
#412=FACE_BOUND('',#2714,.T.);
#413=FACE_BOUND('',#2716,.T.);
#414=FACE_BOUND('',#2717,.T.);
#415=FACE_BOUND('',#2719,.T.);
#416=FACE_BOUND('',#2720,.T.);
#417=FACE_BOUND('',#2722,.T.);
#418=FACE_BOUND('',#2723,.T.);
#419=FACE_BOUND('',#2729,.T.);
#420=FACE_BOUND('',#2731,.T.);
#421=FACE_BOUND('',#2737,.T.);
#422=FACE_BOUND('',#2739,.T.);
#423=FACE_BOUND('',#2749,.T.);
#424=FACE_BOUND('',#2751,.T.);
#425=FACE_BOUND('',#2761,.T.);
#426=FACE_BOUND('',#2763,.T.);
#427=FACE_BOUND('',#2773,.T.);
#428=FACE_BOUND('',#2775,.T.);
#429=FACE_BOUND('',#2785,.T.);
#430=FACE_BOUND('',#2787,.T.);
#431=FACE_BOUND('',#2797,.T.);
#432=FACE_BOUND('',#2799,.T.);
#779=B_SPLINE_CURVE_WITH_KNOTS('',3,(#41011,#41012,#41013,#41014,#41015,
#41016),.UNSPECIFIED.,.F.,.F.,(4,2,4),(0.436494357616827,0.49057908163088,
0.523269669927392),.UNSPECIFIED.);
#780=B_SPLINE_CURVE_WITH_KNOTS('',3,(#41018,#41019,#41020,#41021,#41022,
#41023,#41024,#41025,#41026,#41027,#41028,#41029,#41030,#41031,#41032,#41033,
#41034,#41035,#41036),.UNSPECIFIED.,.F.,.F.,(4,3,3,3,3,3,4),(-1.40481265039417,
-1.36522996541144,-1.32585540726346,-1.28679683363995,-1.26015734748852,
-1.21999608757349,-1.1843388203003),.UNSPECIFIED.);
#781=B_SPLINE_CURVE_WITH_KNOTS('',3,(#41038,#41039,#41040,#41041,#41042,
#41043),.UNSPECIFIED.,.F.,.F.,(4,2,4),(0.436494357616828,0.49057908163088,
0.523269669927516),.UNSPECIFIED.);
#782=B_SPLINE_CURVE_WITH_KNOTS('',3,(#41044,#41045,#41046,#41047,#41048,
#41049,#41050,#41051,#41052,#41053,#41054,#41055,#41056,#41057,#41058,#41059,
#41060,#41061,#41062),.UNSPECIFIED.,.F.,.F.,(4,3,3,3,3,3,4),(1.21344063784114,
1.25510987200879,1.29073244309217,1.33189452838103,1.37317594357341,1.41463545273866,
1.43283480298246),.UNSPECIFIED.);
#783=B_SPLINE_CURVE_WITH_KNOTS('',3,(#41065,#41066,#41067,#41068,#41069,
#41070),.UNSPECIFIED.,.F.,.F.,(4,2,4),(1.43904665659616,1.47173724489264,
1.52582196890669),.UNSPECIFIED.);
#784=B_SPLINE_CURVE_WITH_KNOTS('',3,(#41072,#41073,#41074,#41075,#41076,
#41077,#41078,#41079,#41080,#41081,#41082,#41083,#41084,#41085,#41086,#41087,
#41088,#41089,#41090),.UNSPECIFIED.,.F.,.F.,(4,3,3,3,3,3,4),(2.53632937909178,
2.57775416224765,2.61898206719527,2.6459019021663,2.68717408326041,2.72876559667488,
2.75562831582286),.UNSPECIFIED.);
#785=B_SPLINE_CURVE_WITH_KNOTS('',3,(#41092,#41093,#41094,#41095,#41096,
#41097),.UNSPECIFIED.,.F.,.F.,(4,2,4),(1.43904665659616,1.47173724489264,
1.52582196890582),.UNSPECIFIED.);
#786=B_SPLINE_CURVE_WITH_KNOTS('',3,(#41098,#41099,#41100,#41101,#41102,
#41103,#41104,#41105,#41106,#41107,#41108,#41109,#41110,#41111,#41112,#41113,
#41114,#41115,#41116),.UNSPECIFIED.,.F.,.F.,(4,3,3,3,3,3,4),(-0.110253525235352,
-0.070240741437667,-0.0308586443223014,0.,0.0392000421916667,0.0788707706427855,
0.110060546834446),.UNSPECIFIED.);
#787=B_SPLINE_CURVE_WITH_KNOTS('',3,(#41122,#41123,#41124,#41125,#41126,
#41127),.UNSPECIFIED.,.F.,.F.,(4,2,4),(-1.15327512303049,-1.04744023087766,
-0.941605338724827),.UNSPECIFIED.);
#788=B_SPLINE_CURVE_WITH_KNOTS('',3,(#41131,#41132,#41133,#41134,#41135,
#41136),.UNSPECIFIED.,.F.,.F.,(4,2,4),(0.959836356712345,1.06544831446544,
1.17106027221854),.UNSPECIFIED.);
#789=B_SPLINE_CURVE_WITH_KNOTS('',3,(#41143,#41144,#41145,#41146,#41147,
#41148,#41149),.UNSPECIFIED.,.F.,.F.,(4,3,4),(2.02528467117779,2.13089662893088,
2.23650858668398),.UNSPECIFIED.);
#790=B_SPLINE_CURVE_WITH_KNOTS('',3,(#41153,#41154,#41155,#41156,#41157,
#41158,#41159),.UNSPECIFIED.,.F.,.F.,(4,3,4),(-0.105834892152833,0.,0.105834892152833),
 .UNSPECIFIED.);
#791=B_SPLINE_CURVE_WITH_KNOTS('',3,(#41173,#41174,#41175,#41176,#41177,
#41178),.UNSPECIFIED.,.F.,.F.,(4,2,4),(0.436494357616816,0.49057908163088,
0.523269669927352),.UNSPECIFIED.);
#792=B_SPLINE_CURVE_WITH_KNOTS('',3,(#41180,#41181,#41182,#41183,#41184,
#41185,#41186,#41187,#41188,#41189,#41190,#41191,#41192,#41193,#41194,#41195,
#41196,#41197,#41198),.UNSPECIFIED.,.F.,.F.,(4,3,3,3,3,3,4),(-1.40481265039413,
-1.36522996541145,-1.32585540726349,-1.28679683363998,-1.2601573474885,
-1.21999608757352,-1.18433882030031),.UNSPECIFIED.);
#793=B_SPLINE_CURVE_WITH_KNOTS('',3,(#41200,#41201,#41202,#41203,#41204,
#41205),.UNSPECIFIED.,.F.,.F.,(4,2,4),(0.436484426249651,0.490578640084517,
0.523250481795878),.UNSPECIFIED.);
#794=B_SPLINE_CURVE_WITH_KNOTS('',3,(#41206,#41207,#41208,#41209,#41210,
#41211,#41212,#41213,#41214,#41215,#41216,#41217,#41218,#41219,#41220,#41221,
#41222,#41223,#41224),.UNSPECIFIED.,.F.,.F.,(4,3,3,3,3,3,4),(1.21344063784117,
1.2551098720088,1.29073244309219,1.33189452838105,1.37317594357344,1.41463545273871,
1.43283480298249),.UNSPECIFIED.);
#795=B_SPLINE_CURVE_WITH_KNOTS('',3,(#41227,#41228,#41229,#41230,#41231,
#41232),.UNSPECIFIED.,.F.,.F.,(4,2,4),(1.43906407854219,1.47173592025355,
1.52583013408841),.UNSPECIFIED.);
#796=B_SPLINE_CURVE_WITH_KNOTS('',3,(#41234,#41235,#41236,#41237,#41238,
#41239,#41240,#41241,#41242,#41243,#41244,#41245,#41246,#41247,#41248,#41249,
#41250,#41251,#41252),.UNSPECIFIED.,.F.,.F.,(4,3,3,3,3,3,4),(2.53632937909181,
2.57775416224765,2.61898206719527,2.64590190216633,2.68717408326044,2.72876559667489,
2.75562831582288),.UNSPECIFIED.);
#797=B_SPLINE_CURVE_WITH_KNOTS('',3,(#41254,#41255,#41256,#41257,#41258,
#41259),.UNSPECIFIED.,.F.,.F.,(4,2,4),(1.43906407854219,1.47173592025355,
1.52583013408754),.UNSPECIFIED.);
#798=B_SPLINE_CURVE_WITH_KNOTS('',3,(#41260,#41261,#41262,#41263,#41264,
#41265,#41266,#41267,#41268,#41269,#41270,#41271,#41272,#41273,#41274,#41275,
#41276,#41277,#41278),.UNSPECIFIED.,.F.,.F.,(4,3,3,3,3,3,4),(-0.110253525235351,
-0.0702407414376934,-0.0308586443223274,0.,0.0392000421916682,0.0788707706427895,
0.110060546834446),.UNSPECIFIED.);
#799=B_SPLINE_CURVE_WITH_KNOTS('',3,(#41284,#41285,#41286,#41287,#41288,
#41289),.UNSPECIFIED.,.F.,.F.,(4,2,4),(-1.15327512303049,-1.04744023087766,
-0.941605338724829),.UNSPECIFIED.);
#800=B_SPLINE_CURVE_WITH_KNOTS('',3,(#41293,#41294,#41295,#41296,#41297,
#41298),.UNSPECIFIED.,.F.,.F.,(4,2,4),(0.959836356712343,1.06544831446544,
1.17106027221854),.UNSPECIFIED.);
#801=B_SPLINE_CURVE_WITH_KNOTS('',3,(#41305,#41306,#41307,#41308,#41309,
#41310,#41311),.UNSPECIFIED.,.F.,.F.,(4,3,4),(2.02528467117778,2.13089662893088,
2.23650858668398),.UNSPECIFIED.);
#802=B_SPLINE_CURVE_WITH_KNOTS('',3,(#41315,#41316,#41317,#41318,#41319,
#41320,#41321),.UNSPECIFIED.,.F.,.F.,(4,3,4),(-0.105834892152834,0.,0.105834892152833),
 .UNSPECIFIED.);
#803=B_SPLINE_CURVE_WITH_KNOTS('',3,(#41335,#41336,#41337,#41338,#41339,
#41340),.UNSPECIFIED.,.F.,.F.,(4,2,4),(0.436484426249655,0.490578640084517,
0.523250481795882),.UNSPECIFIED.);
#804=B_SPLINE_CURVE_WITH_KNOTS('',3,(#41342,#41343,#41344,#41345,#41346,
#41347,#41348,#41349,#41350,#41351,#41352,#41353,#41354,#41355,#41356,#41357,
#41358,#41359,#41360),.UNSPECIFIED.,.F.,.F.,(4,3,3,3,3,3,4),(-0.110253525235353,
-0.0702407414376493,-0.0308586443222864,0.,0.0392000421916586,0.0788707706427754,
0.110060546834447),.UNSPECIFIED.);
#805=B_SPLINE_CURVE_WITH_KNOTS('',3,(#41362,#41363,#41364,#41365,#41366,
#41367),.UNSPECIFIED.,.F.,.F.,(4,2,4),(0.436494357616821,0.49057908163088,
0.523269669927365),.UNSPECIFIED.);
#806=B_SPLINE_CURVE_WITH_KNOTS('',3,(#41368,#41369,#41370,#41371,#41372,
#41373,#41374,#41375,#41376,#41377,#41378,#41379,#41380,#41381,#41382,#41383,
#41384,#41385,#41386),.UNSPECIFIED.,.F.,.F.,(4,3,3,3,3,3,4),(2.53632937909178,
2.57775416224762,2.61898206719525,2.64590190216632,2.68717408326042,2.72876559667488,
2.75562831582289),.UNSPECIFIED.);
#807=B_SPLINE_CURVE_WITH_KNOTS('',3,(#41389,#41390,#41391,#41392,#41393,
#41394),.UNSPECIFIED.,.F.,.F.,(4,2,4),(1.43906407854219,1.47173592025355,
1.52583013408841),.UNSPECIFIED.);
#808=B_SPLINE_CURVE_WITH_KNOTS('',3,(#41396,#41397,#41398,#41399,#41400,
#41401,#41402,#41403,#41404,#41405,#41406,#41407,#41408,#41409,#41410,#41411,
#41412,#41413,#41414),.UNSPECIFIED.,.F.,.F.,(4,3,3,3,3,3,4),(1.21344063784118,
1.25510987200885,1.29073244309219,1.33189452838105,1.37317594357345,1.41463545273868,
1.43283480298247),.UNSPECIFIED.);
#809=B_SPLINE_CURVE_WITH_KNOTS('',3,(#41416,#41417,#41418,#41419,#41420,
#41421),.UNSPECIFIED.,.F.,.F.,(4,2,4),(1.43906407854219,1.47173592025355,
1.52583013408753),.UNSPECIFIED.);
#810=B_SPLINE_CURVE_WITH_KNOTS('',3,(#41422,#41423,#41424,#41425,#41426,
#41427,#41428,#41429,#41430,#41431,#41432,#41433,#41434,#41435,#41436,#41437,
#41438,#41439,#41440),.UNSPECIFIED.,.F.,.F.,(4,3,3,3,3,3,4),(-1.40481265039415,
-1.36522996541142,-1.32585540726345,-1.28679683363994,-1.26015734748852,
-1.21999608757345,-1.18433882030032),.UNSPECIFIED.);
#811=B_SPLINE_CURVE_WITH_KNOTS('',3,(#41446,#41447,#41448,#41449,#41450,
#41451),.UNSPECIFIED.,.F.,.F.,(4,2,4),(-1.15327512303049,-1.04744023087766,
-0.941605338724827),.UNSPECIFIED.);
#812=B_SPLINE_CURVE_WITH_KNOTS('',3,(#41455,#41456,#41457,#41458,#41459,
#41460),.UNSPECIFIED.,.F.,.F.,(4,2,4),(0.959836356712344,1.06544831446544,
1.17106027221854),.UNSPECIFIED.);
#813=B_SPLINE_CURVE_WITH_KNOTS('',3,(#41467,#41468,#41469,#41470,#41471,
#41472,#41473),.UNSPECIFIED.,.F.,.F.,(4,3,4),(2.02528467117779,2.13089662893088,
2.23650858668398),.UNSPECIFIED.);
#814=B_SPLINE_CURVE_WITH_KNOTS('',3,(#41477,#41478,#41479,#41480,#41481,
#41482,#41483),.UNSPECIFIED.,.F.,.F.,(4,3,4),(-0.105834892152832,0.,0.105834892152832),
 .UNSPECIFIED.);
#815=B_SPLINE_CURVE_WITH_KNOTS('',3,(#41497,#41498,#41499,#41500,#41501,
#41502),.UNSPECIFIED.,.F.,.F.,(4,2,4),(0.436494357616822,0.49057908163088,
0.523269669927398),.UNSPECIFIED.);
#816=B_SPLINE_CURVE_WITH_KNOTS('',3,(#41504,#41505,#41506,#41507,#41508,
#41509,#41510,#41511,#41512,#41513,#41514,#41515,#41516,#41517,#41518,#41519,
#41520,#41521,#41522),.UNSPECIFIED.,.F.,.F.,(4,3,3,3,3,3,4),(-0.110253525235377,
-0.070240741437708,-0.0308586443223363,0.,0.03920004219167,0.0788707706428437,
0.110060546834472),.UNSPECIFIED.);
#817=B_SPLINE_CURVE_WITH_KNOTS('',3,(#41524,#41525,#41526,#41527,#41528,
#41529),.UNSPECIFIED.,.F.,.F.,(4,2,4),(0.436484426249657,0.490578640084517,
0.523250481796065),.UNSPECIFIED.);
#818=B_SPLINE_CURVE_WITH_KNOTS('',3,(#41530,#41531,#41532,#41533,#41534,
#41535,#41536,#41537,#41538,#41539,#41540,#41541,#41542,#41543,#41544,#41545,
#41546,#41547,#41548),.UNSPECIFIED.,.F.,.F.,(4,3,3,3,3,3,4),(2.53632937909185,
2.57775416224773,2.61898206719535,2.64590190216638,2.6871740832605,2.72876559667492,
2.75562831582295),.UNSPECIFIED.);
#819=B_SPLINE_CURVE_WITH_KNOTS('',3,(#41551,#41552,#41553,#41554,#41555,
#41556),.UNSPECIFIED.,.F.,.F.,(4,2,4),(1.43904665659616,1.47173724489264,
1.52582196890669),.UNSPECIFIED.);
#820=B_SPLINE_CURVE_WITH_KNOTS('',3,(#41558,#41559,#41560,#41561,#41562,
#41563,#41564,#41565,#41566,#41567,#41568,#41569,#41570,#41571,#41572,#41573,
#41574,#41575,#41576),.UNSPECIFIED.,.F.,.F.,(4,3,3,3,3,3,4),(1.2134406378412,
1.25510987200883,1.29073244309221,1.33189452838107,1.37317594357346,1.41463545273868,
1.43283480298249),.UNSPECIFIED.);
#821=B_SPLINE_CURVE_WITH_KNOTS('',3,(#41578,#41579,#41580,#41581,#41582,
#41583),.UNSPECIFIED.,.F.,.F.,(4,2,4),(1.43904665659616,1.47173724489264,
1.52582196890583),.UNSPECIFIED.);
#822=B_SPLINE_CURVE_WITH_KNOTS('',3,(#41584,#41585,#41586,#41587,#41588,
#41589,#41590,#41591,#41592,#41593,#41594,#41595,#41596,#41597,#41598,#41599,
#41600,#41601,#41602),.UNSPECIFIED.,.F.,.F.,(4,3,3,3,3,3,4),(-1.40481265039411,
-1.36522996541141,-1.32585540726345,-1.28679683363994,-1.26015734748849,
-1.21999608757351,-1.1843388203003),.UNSPECIFIED.);
#823=B_SPLINE_CURVE_WITH_KNOTS('',3,(#41608,#41609,#41610,#41611,#41612,
#41613),.UNSPECIFIED.,.F.,.F.,(4,2,4),(-1.15327512303049,-1.04744023087766,
-0.941605338724826),.UNSPECIFIED.);
#824=B_SPLINE_CURVE_WITH_KNOTS('',3,(#41617,#41618,#41619,#41620,#41621,
#41622),.UNSPECIFIED.,.F.,.F.,(4,2,4),(0.959836356712345,1.06544831446544,
1.17106027221854),.UNSPECIFIED.);
#825=B_SPLINE_CURVE_WITH_KNOTS('',3,(#41629,#41630,#41631,#41632,#41633,
#41634,#41635),.UNSPECIFIED.,.F.,.F.,(4,3,4),(2.02528467117779,2.13089662893088,
2.23650858668398),.UNSPECIFIED.);
#826=B_SPLINE_CURVE_WITH_KNOTS('',3,(#41639,#41640,#41641,#41642,#41643,
#41644,#41645),.UNSPECIFIED.,.F.,.F.,(4,3,4),(-0.105834892152833,0.,0.105834892152832),
 .UNSPECIFIED.);
#827=B_SPLINE_CURVE_WITH_KNOTS('',3,(#41659,#41660,#41661,#41662,#41663,
#41664),.UNSPECIFIED.,.F.,.F.,(4,2,4),(0.436494357616821,0.49057908163088,
0.523269669927355),.UNSPECIFIED.);
#828=B_SPLINE_CURVE_WITH_KNOTS('',3,(#41666,#41667,#41668,#41669,#41670,
#41671,#41672,#41673,#41674,#41675,#41676,#41677,#41678,#41679,#41680,#41681,
#41682,#41683,#41684),.UNSPECIFIED.,.F.,.F.,(4,3,3,3,3,3,4),(-0.110253525235352,
-0.0702407414377446,-0.0308586443223844,0.,0.039200042191676,0.0788707706427867,
0.110060546834448),.UNSPECIFIED.);
#829=B_SPLINE_CURVE_WITH_KNOTS('',3,(#41686,#41687,#41688,#41689,#41690,
#41691),.UNSPECIFIED.,.F.,.F.,(4,2,4),(0.436494357616821,0.49057908163088,
0.523269669927355),.UNSPECIFIED.);
#830=B_SPLINE_CURVE_WITH_KNOTS('',3,(#41692,#41693,#41694,#41695,#41696,
#41697,#41698,#41699,#41700,#41701,#41702,#41703,#41704,#41705,#41706,#41707,
#41708,#41709,#41710),.UNSPECIFIED.,.F.,.F.,(4,3,3,3,3,3,4),(2.53632937909179,
2.57775416224772,2.61898206719534,2.64590190216632,2.68717408326042,2.72876559667486,
2.75562831582289),.UNSPECIFIED.);
#831=B_SPLINE_CURVE_WITH_KNOTS('',3,(#41713,#41714,#41715,#41716,#41717,
#41718),.UNSPECIFIED.,.F.,.F.,(4,2,4),(1.43904665659616,1.47173724489264,
1.5258219689067),.UNSPECIFIED.);
#832=B_SPLINE_CURVE_WITH_KNOTS('',3,(#41720,#41721,#41722,#41723,#41724,
#41725,#41726,#41727,#41728,#41729,#41730,#41731,#41732,#41733,#41734,#41735,
#41736,#41737,#41738),.UNSPECIFIED.,.F.,.F.,(4,3,3,3,3,3,4),(1.21344063784118,
1.25510987200879,1.29073244309219,1.33189452838105,1.37317594357344,1.41463545273868,
1.43283480298247),.UNSPECIFIED.);
#833=B_SPLINE_CURVE_WITH_KNOTS('',3,(#41740,#41741,#41742,#41743,#41744,
#41745),.UNSPECIFIED.,.F.,.F.,(4,2,4),(1.43904665659616,1.47173724489264,
1.52582196890582),.UNSPECIFIED.);
#834=B_SPLINE_CURVE_WITH_KNOTS('',3,(#41746,#41747,#41748,#41749,#41750,
#41751,#41752,#41753,#41754,#41755,#41756,#41757,#41758,#41759,#41760,#41761,
#41762,#41763,#41764),.UNSPECIFIED.,.F.,.F.,(4,3,3,3,3,3,4),(-1.40481265039416,
-1.36522996541145,-1.32585540726348,-1.28679683363997,-1.26015734748853,
-1.21999608757355,-1.18433882030033),.UNSPECIFIED.);
#835=B_SPLINE_CURVE_WITH_KNOTS('',3,(#41770,#41771,#41772,#41773,#41774,
#41775),.UNSPECIFIED.,.F.,.F.,(4,2,4),(-1.15327512303049,-1.04744023087766,
-0.941605338724826),.UNSPECIFIED.);
#836=B_SPLINE_CURVE_WITH_KNOTS('',3,(#41779,#41780,#41781,#41782,#41783,
#41784),.UNSPECIFIED.,.F.,.F.,(4,2,4),(0.959836356712344,1.06544831446544,
1.17106027221854),.UNSPECIFIED.);
#837=B_SPLINE_CURVE_WITH_KNOTS('',3,(#41791,#41792,#41793,#41794,#41795,
#41796,#41797),.UNSPECIFIED.,.F.,.F.,(4,3,4),(2.02528467117778,2.13089662893088,
2.23650858668398),.UNSPECIFIED.);
#838=B_SPLINE_CURVE_WITH_KNOTS('',3,(#41801,#41802,#41803,#41804,#41805,
#41806,#41807),.UNSPECIFIED.,.F.,.F.,(4,3,4),(-0.105834892152833,0.,0.105834892152832),
 .UNSPECIFIED.);
#839=B_SPLINE_CURVE_WITH_KNOTS('',3,(#41821,#41822,#41823,#41824,#41825,
#41826,#41827,#41828,#41829,#41830,#41831,#41832,#41833,#41834,#41835,#41836,
#41837,#41838,#41839),.UNSPECIFIED.,.F.,.F.,(4,3,3,3,3,3,4),(2.47883976068978,
2.51859129056809,2.55786629068885,2.58890030752247,2.62818560996811,2.66809093310445,
2.69915383275782),.UNSPECIFIED.);
#840=B_SPLINE_CURVE_WITH_KNOTS('',3,(#41841,#41842,#41843,#41844,#41845,
#41846),.UNSPECIFIED.,.F.,.F.,(4,2,4),(-0.523250481795879,-0.490578640084517,
-0.43648442624966),.UNSPECIFIED.);
#841=B_SPLINE_CURVE_WITH_KNOTS('',3,(#41848,#41849,#41850,#41851,#41852,
#41853,#41854,#41855,#41856,#41857,#41858,#41859,#41860,#41861,#41862,#41863,
#41864,#41865,#41866),.UNSPECIFIED.,.F.,.F.,(4,3,3,3,3,3,4),(-0.109726413656553,
-0.0680893754924848,-0.0267736956128723,0.,0.0412006233150074,0.082597721206199,
0.109572523074534),.UNSPECIFIED.);
#842=B_SPLINE_CURVE_WITH_KNOTS('',3,(#41867,#41868,#41869,#41870,#41871,
#41872),.UNSPECIFIED.,.F.,.F.,(4,2,4),(-0.523250481795672,-0.490578640084517,
-0.436484426249653),.UNSPECIFIED.);
#843=B_SPLINE_CURVE_WITH_KNOTS('',3,(#41875,#41876,#41877,#41878,#41879,
#41880),.UNSPECIFIED.,.F.,.F.,(4,2,4),(1.43904665659616,1.47173724489264,
1.5258219689067),.UNSPECIFIED.);
#844=B_SPLINE_CURVE_WITH_KNOTS('',3,(#41882,#41883,#41884,#41885,#41886,
#41887,#41888,#41889,#41890,#41891,#41892,#41893,#41894,#41895,#41896,#41897,
#41898,#41899,#41900),.UNSPECIFIED.,.F.,.F.,(4,3,3,3,3,3,4),(1.21344063784118,
1.25510987200878,1.29073244309219,1.33189452838105,1.37317594357344,1.41463545273868,
1.43283480298247),.UNSPECIFIED.);
#845=B_SPLINE_CURVE_WITH_KNOTS('',3,(#41902,#41903,#41904,#41905,#41906,
#41907),.UNSPECIFIED.,.F.,.F.,(4,2,4),(1.43904665659617,1.47173724489264,
1.52582196890583),.UNSPECIFIED.);
#846=B_SPLINE_CURVE_WITH_KNOTS('',3,(#41908,#41909,#41910,#41911,#41912,
#41913,#41914,#41915,#41916,#41917,#41918,#41919,#41920,#41921,#41922,#41923,
#41924,#41925,#41926),.UNSPECIFIED.,.F.,.F.,(4,3,3,3,3,3,4),(-1.40481265039414,
-1.36522996541144,-1.32585540726348,-1.28679683363997,-1.26015734748851,
-1.21999608757358,-1.18433882030032),.UNSPECIFIED.);
#847=B_SPLINE_CURVE_WITH_KNOTS('',3,(#41936,#41937,#41938,#41939,#41940,
#41941,#41942),.UNSPECIFIED.,.F.,.F.,(4,3,4),(2.02528467117778,2.13089662893088,
2.23650858668398),.UNSPECIFIED.);
#848=B_SPLINE_CURVE_WITH_KNOTS('',3,(#41946,#41947,#41948,#41949,#41950,
#41951,#41952),.UNSPECIFIED.,.F.,.F.,(4,3,4),(-0.105834892152832,0.,0.105834892152832),
 .UNSPECIFIED.);
#849=B_SPLINE_CURVE_WITH_KNOTS('',3,(#41957,#41958,#41959,#41960,#41961,
#41962),.UNSPECIFIED.,.F.,.F.,(4,2,4),(0.941605338724826,1.04744023087766,
1.15327512303049),.UNSPECIFIED.);
#850=B_SPLINE_CURVE_WITH_KNOTS('',3,(#41965,#41966,#41967,#41968,#41969,
#41970),.UNSPECIFIED.,.F.,.F.,(4,2,4),(-1.17106027221854,-1.06544831446544,
-0.959836356712344),.UNSPECIFIED.);
#851=B_SPLINE_CURVE_WITH_KNOTS('',3,(#41980,#41981,#41982,#41983,#41984,
#41985),.UNSPECIFIED.,.F.,.F.,(4,2,4),(-1.15327512303049,-1.04744023087766,
-0.941605338724827),.UNSPECIFIED.);
#852=B_SPLINE_CURVE_WITH_KNOTS('',3,(#41989,#41990,#41991,#41992,#41993,
#41994),.UNSPECIFIED.,.F.,.F.,(4,2,4),(0.959836356712344,1.06544831446544,
1.17106027221854),.UNSPECIFIED.);
#853=B_SPLINE_CURVE_WITH_KNOTS('',3,(#42001,#42002,#42003,#42004,#42005,
#42006,#42007),.UNSPECIFIED.,.F.,.F.,(4,3,4),(2.02528467117778,2.13089662893088,
2.23650858668398),.UNSPECIFIED.);
#854=B_SPLINE_CURVE_WITH_KNOTS('',3,(#42011,#42012,#42013,#42014,#42015,
#42016,#42017),.UNSPECIFIED.,.F.,.F.,(4,3,4),(-0.105834892152833,0.,0.105834892152832),
 .UNSPECIFIED.);
#855=B_SPLINE_CURVE_WITH_KNOTS('',3,(#42031,#42032,#42033,#42034,#42035,
#42036),.UNSPECIFIED.,.F.,.F.,(4,2,4),(0.43648442624966,0.490578640084517,
0.523250481795913),.UNSPECIFIED.);
#856=B_SPLINE_CURVE_WITH_KNOTS('',3,(#42038,#42039,#42040,#42041,#42042,
#42043,#42044,#42045,#42046,#42047,#42048,#42049,#42050,#42051,#42052,#42053,
#42054,#42055,#42056),.UNSPECIFIED.,.F.,.F.,(4,3,3,3,3,3,4),(-1.40481265039423,
-1.36522996541152,-1.32585540726357,-1.28679683364005,-1.26015734748857,
-1.2199960875736,-1.18433882030035),.UNSPECIFIED.);
#857=B_SPLINE_CURVE_WITH_KNOTS('',3,(#42058,#42059,#42060,#42061,#42062,
#42063),.UNSPECIFIED.,.F.,.F.,(4,2,4),(0.436494357616825,0.49057908163088,
0.523269669927497),.UNSPECIFIED.);
#858=B_SPLINE_CURVE_WITH_KNOTS('',3,(#42064,#42065,#42066,#42067,#42068,
#42069,#42070,#42071,#42072,#42073,#42074,#42075,#42076,#42077,#42078,#42079,
#42080,#42081,#42082),.UNSPECIFIED.,.F.,.F.,(4,3,3,3,3,3,4),(1.21344063784115,
1.25510987200874,1.29073244309218,1.33189452838104,1.37317594357343,1.41463545273866,
1.43283480298248),.UNSPECIFIED.);
#859=B_SPLINE_CURVE_WITH_KNOTS('',3,(#42085,#42086,#42087,#42088,#42089,
#42090),.UNSPECIFIED.,.F.,.F.,(4,2,4),(1.43906407854219,1.47173592025355,
1.52583013408841),.UNSPECIFIED.);
#860=B_SPLINE_CURVE_WITH_KNOTS('',3,(#42092,#42093,#42094,#42095,#42096,
#42097,#42098,#42099,#42100,#42101,#42102,#42103,#42104,#42105,#42106,#42107,
#42108,#42109,#42110),.UNSPECIFIED.,.F.,.F.,(4,3,3,3,3,3,4),(2.53632937909179,
2.57775416224768,2.61898206719531,2.64590190216631,2.68717408326042,2.72876559667485,
2.75562831582286),.UNSPECIFIED.);
#861=B_SPLINE_CURVE_WITH_KNOTS('',3,(#42112,#42113,#42114,#42115,#42116,
#42117),.UNSPECIFIED.,.F.,.F.,(4,2,4),(1.43906407854219,1.47173592025355,
1.52583013408754),.UNSPECIFIED.);
#862=B_SPLINE_CURVE_WITH_KNOTS('',3,(#42118,#42119,#42120,#42121,#42122,
#42123,#42124,#42125,#42126,#42127,#42128,#42129,#42130,#42131,#42132,#42133,
#42134,#42135,#42136),.UNSPECIFIED.,.F.,.F.,(4,3,3,3,3,3,4),(-0.110253525235352,
-0.0702407414376601,-0.030858644322292,0.,0.0392000421916706,0.0788707706427867,
0.110060546834447),.UNSPECIFIED.);
#1175=PLANE('',#14278);
#1176=PLANE('',#14279);
#1177=PLANE('',#14336);
#1178=PLANE('',#14337);
#1179=PLANE('',#14338);
#1180=PLANE('',#14339);
#1181=PLANE('',#14340);
#1182=PLANE('',#14341);
#1183=PLANE('',#14446);
#1184=PLANE('',#14447);
#1185=PLANE('',#14448);
#1186=PLANE('',#14449);
#1187=PLANE('',#14450);
#1188=PLANE('',#14453);
#1189=PLANE('',#14458);
#1190=PLANE('',#14459);
#1191=PLANE('',#14460);
#1192=PLANE('',#14463);
#1193=PLANE('',#14474);
#1194=PLANE('',#14475);
#1195=PLANE('',#14476);
#1196=PLANE('',#14477);
#1197=PLANE('',#14478);
#1198=PLANE('',#14481);
#1199=PLANE('',#14492);
#1200=PLANE('',#14493);
#1201=PLANE('',#14494);
#1202=PLANE('',#14495);
#1203=PLANE('',#14496);
#1204=PLANE('',#14499);
#1205=PLANE('',#14510);
#1206=PLANE('',#14511);
#1207=PLANE('',#14512);
#1208=PLANE('',#14513);
#1209=PLANE('',#14514);
#1210=PLANE('',#14517);
#1211=PLANE('',#14528);
#1212=PLANE('',#14529);
#1213=PLANE('',#14530);
#1214=PLANE('',#14531);
#1215=PLANE('',#14532);
#1216=PLANE('',#14535);
#1217=PLANE('',#14546);
#1218=PLANE('',#14547);
#1219=PLANE('',#14548);
#1220=PLANE('',#14549);
#1221=PLANE('',#14550);
#1222=PLANE('',#14553);
#1223=PLANE('',#14558);
#1224=PLANE('',#14561);
#1781=FACE_OUTER_BOUND('',#2637,.T.);
#1782=FACE_OUTER_BOUND('',#2638,.T.);
#1783=FACE_OUTER_BOUND('',#2639,.T.);
#1784=FACE_OUTER_BOUND('',#2640,.T.);
#1785=FACE_OUTER_BOUND('',#2641,.T.);
#1786=FACE_OUTER_BOUND('',#2642,.T.);
#1787=FACE_OUTER_BOUND('',#2643,.T.);
#1788=FACE_OUTER_BOUND('',#2644,.T.);
#1789=FACE_OUTER_BOUND('',#2645,.T.);
#1790=FACE_OUTER_BOUND('',#2647,.T.);
#1791=FACE_OUTER_BOUND('',#2649,.T.);
#1792=FACE_OUTER_BOUND('',#2650,.T.);
#1793=FACE_OUTER_BOUND('',#2651,.T.);
#1794=FACE_OUTER_BOUND('',#2652,.T.);
#1795=FACE_OUTER_BOUND('',#2653,.T.);
#1796=FACE_OUTER_BOUND('',#2654,.T.);
#1797=FACE_OUTER_BOUND('',#2655,.T.);
#1798=FACE_OUTER_BOUND('',#2656,.T.);
#1799=FACE_OUTER_BOUND('',#2657,.T.);
#1800=FACE_OUTER_BOUND('',#2658,.T.);
#1801=FACE_OUTER_BOUND('',#2659,.T.);
#1802=FACE_OUTER_BOUND('',#2660,.T.);
#1803=FACE_OUTER_BOUND('',#2661,.T.);
#1804=FACE_OUTER_BOUND('',#2662,.T.);
#1805=FACE_OUTER_BOUND('',#2663,.T.);
#1806=FACE_OUTER_BOUND('',#2664,.T.);
#1807=FACE_OUTER_BOUND('',#2665,.T.);
#1808=FACE_OUTER_BOUND('',#2666,.T.);
#1809=FACE_OUTER_BOUND('',#2667,.T.);
#1810=FACE_OUTER_BOUND('',#2668,.T.);
#1811=FACE_OUTER_BOUND('',#2669,.T.);
#1812=FACE_OUTER_BOUND('',#2670,.T.);
#1813=FACE_OUTER_BOUND('',#2672,.T.);
#1814=FACE_OUTER_BOUND('',#2674,.T.);
#1815=FACE_OUTER_BOUND('',#2676,.T.);
#1816=FACE_OUTER_BOUND('',#2678,.T.);
#1817=FACE_OUTER_BOUND('',#2680,.T.);
#1818=FACE_OUTER_BOUND('',#2682,.T.);
#1819=FACE_OUTER_BOUND('',#2685,.T.);
#1820=FACE_OUTER_BOUND('',#2688,.T.);
#1821=FACE_OUTER_BOUND('',#2691,.T.);
#1822=FACE_OUTER_BOUND('',#2694,.T.);
#1823=FACE_OUTER_BOUND('',#2697,.T.);
#1824=FACE_OUTER_BOUND('',#2700,.T.);
#1825=FACE_OUTER_BOUND('',#2703,.T.);
#1826=FACE_OUTER_BOUND('',#2706,.T.);
#1827=FACE_OUTER_BOUND('',#2709,.T.);
#1828=FACE_OUTER_BOUND('',#2712,.T.);
#1829=FACE_OUTER_BOUND('',#2715,.T.);
#1830=FACE_OUTER_BOUND('',#2718,.T.);
#1831=FACE_OUTER_BOUND('',#2721,.T.);
#1832=FACE_OUTER_BOUND('',#2724,.T.);
#1833=FACE_OUTER_BOUND('',#2725,.T.);
#1834=FACE_OUTER_BOUND('',#2726,.T.);
#1835=FACE_OUTER_BOUND('',#2727,.T.);
#1836=FACE_OUTER_BOUND('',#2728,.T.);
#1837=FACE_OUTER_BOUND('',#2730,.T.);
#1838=FACE_OUTER_BOUND('',#2732,.T.);
#1839=FACE_OUTER_BOUND('',#2733,.T.);
#1840=FACE_OUTER_BOUND('',#2734,.T.);
#1841=FACE_OUTER_BOUND('',#2735,.T.);
#1842=FACE_OUTER_BOUND('',#2736,.T.);
#1843=FACE_OUTER_BOUND('',#2738,.T.);
#1844=FACE_OUTER_BOUND('',#2740,.T.);
#1845=FACE_OUTER_BOUND('',#2741,.T.);
#1846=FACE_OUTER_BOUND('',#2742,.T.);
#1847=FACE_OUTER_BOUND('',#2743,.T.);
#1848=FACE_OUTER_BOUND('',#2744,.T.);
#1849=FACE_OUTER_BOUND('',#2745,.T.);
#1850=FACE_OUTER_BOUND('',#2746,.T.);
#1851=FACE_OUTER_BOUND('',#2747,.T.);
#1852=FACE_OUTER_BOUND('',#2748,.T.);
#1853=FACE_OUTER_BOUND('',#2750,.T.);
#1854=FACE_OUTER_BOUND('',#2752,.T.);
#1855=FACE_OUTER_BOUND('',#2753,.T.);
#1856=FACE_OUTER_BOUND('',#2754,.T.);
#1857=FACE_OUTER_BOUND('',#2755,.T.);
#1858=FACE_OUTER_BOUND('',#2756,.T.);
#1859=FACE_OUTER_BOUND('',#2757,.T.);
#1860=FACE_OUTER_BOUND('',#2758,.T.);
#1861=FACE_OUTER_BOUND('',#2759,.T.);
#1862=FACE_OUTER_BOUND('',#2760,.T.);
#1863=FACE_OUTER_BOUND('',#2762,.T.);
#1864=FACE_OUTER_BOUND('',#2764,.T.);
#1865=FACE_OUTER_BOUND('',#2765,.T.);
#1866=FACE_OUTER_BOUND('',#2766,.T.);
#1867=FACE_OUTER_BOUND('',#2767,.T.);
#1868=FACE_OUTER_BOUND('',#2768,.T.);
#1869=FACE_OUTER_BOUND('',#2769,.T.);
#1870=FACE_OUTER_BOUND('',#2770,.T.);
#1871=FACE_OUTER_BOUND('',#2771,.T.);
#1872=FACE_OUTER_BOUND('',#2772,.T.);
#1873=FACE_OUTER_BOUND('',#2774,.T.);
#1874=FACE_OUTER_BOUND('',#2776,.T.);
#1875=FACE_OUTER_BOUND('',#2777,.T.);
#1876=FACE_OUTER_BOUND('',#2778,.T.);
#1877=FACE_OUTER_BOUND('',#2779,.T.);
#1878=FACE_OUTER_BOUND('',#2780,.T.);
#1879=FACE_OUTER_BOUND('',#2781,.T.);
#1880=FACE_OUTER_BOUND('',#2782,.T.);
#1881=FACE_OUTER_BOUND('',#2783,.T.);
#1882=FACE_OUTER_BOUND('',#2784,.T.);
#1883=FACE_OUTER_BOUND('',#2786,.T.);
#1884=FACE_OUTER_BOUND('',#2788,.T.);
#1885=FACE_OUTER_BOUND('',#2789,.T.);
#1886=FACE_OUTER_BOUND('',#2790,.T.);
#1887=FACE_OUTER_BOUND('',#2791,.T.);
#1888=FACE_OUTER_BOUND('',#2792,.T.);
#1889=FACE_OUTER_BOUND('',#2793,.T.);
#1890=FACE_OUTER_BOUND('',#2794,.T.);
#1891=FACE_OUTER_BOUND('',#2795,.T.);
#1892=FACE_OUTER_BOUND('',#2796,.T.);
#1893=FACE_OUTER_BOUND('',#2798,.T.);
#1894=FACE_OUTER_BOUND('',#2800,.T.);
#1895=FACE_OUTER_BOUND('',#2801,.T.);
#1896=FACE_OUTER_BOUND('',#2802,.T.);
#1897=FACE_OUTER_BOUND('',#2803,.T.);
#1898=FACE_OUTER_BOUND('',#2804,.T.);
#1899=FACE_OUTER_BOUND('',#2805,.T.);
#1900=FACE_OUTER_BOUND('',#2806,.T.);
#1901=FACE_OUTER_BOUND('',#2807,.T.);
#2637=EDGE_LOOP('',(#10791,#10792,#10793,#10794));
#2638=EDGE_LOOP('',(#10795,#10796,#10797,#10798,#10799,#10800));
#2639=EDGE_LOOP('',(#10801,#10802,#10803,#10804,#10805));
#2640=EDGE_LOOP('',(#10806,#10807,#10808,#10809,#10810));
#2641=EDGE_LOOP('',(#10811,#10812,#10813,#10814,#10815,#10816));
#2642=EDGE_LOOP('',(#10817,#10818,#10819,#10820));
#2643=EDGE_LOOP('',(#10821,#10822,#10823,#10824));
#2644=EDGE_LOOP('',(#10825,#10826,#10827,#10828));
#2645=EDGE_LOOP('',(#10829));
#2646=EDGE_LOOP('',(#10830));
#2647=EDGE_LOOP('',(#10831));
#2648=EDGE_LOOP('',(#10832));
#2649=EDGE_LOOP('',(#10833,#10834));
#2650=EDGE_LOOP('',(#10835,#10836));
#2651=EDGE_LOOP('',(#10837,#10838));
#2652=EDGE_LOOP('',(#10839,#10840));
#2653=EDGE_LOOP('',(#10841,#10842));
#2654=EDGE_LOOP('',(#10843,#10844));
#2655=EDGE_LOOP('',(#10845,#10846));
#2656=EDGE_LOOP('',(#10847,#10848,#10849,#10850,#10851));
#2657=EDGE_LOOP('',(#10852,#10853,#10854,#10855));
#2658=EDGE_LOOP('',(#10856,#10857,#10858,#10859));
#2659=EDGE_LOOP('',(#10860,#10861,#10862,#10863,#10864));
#2660=EDGE_LOOP('',(#10865,#10866,#10867,#10868));
#2661=EDGE_LOOP('',(#10869,#10870,#10871,#10872,#10873));
#2662=EDGE_LOOP('',(#10874,#10875,#10876,#10877,#10878));
#2663=EDGE_LOOP('',(#10879,#10880,#10881,#10882));
#2664=EDGE_LOOP('',(#10883,#10884,#10885,#10886));
#2665=EDGE_LOOP('',(#10887,#10888,#10889,#10890));
#2666=EDGE_LOOP('',(#10891,#10892,#10893,#10894));
#2667=EDGE_LOOP('',(#10895,#10896,#10897,#10898));
#2668=EDGE_LOOP('',(#10899,#10900,#10901,#10902,#10903));
#2669=EDGE_LOOP('',(#10904,#10905,#10906,#10907,#10908));
#2670=EDGE_LOOP('',(#10909));
#2671=EDGE_LOOP('',(#10910));
#2672=EDGE_LOOP('',(#10911));
#2673=EDGE_LOOP('',(#10912));
#2674=EDGE_LOOP('',(#10913));
#2675=EDGE_LOOP('',(#10914));
#2676=EDGE_LOOP('',(#10915));
#2677=EDGE_LOOP('',(#10916));
#2678=EDGE_LOOP('',(#10917));
#2679=EDGE_LOOP('',(#10918));
#2680=EDGE_LOOP('',(#10919));
#2681=EDGE_LOOP('',(#10920));
#2682=EDGE_LOOP('',(#10921,#10922,#10923,#10924));
#2683=EDGE_LOOP('',(#10925,#10926,#10927,#10928));
#2684=EDGE_LOOP('',(#10929,#10930,#10931,#10932));
#2685=EDGE_LOOP('',(#10933,#10934,#10935,#10936,#10937,#10938,#10939,#10940,
#10941,#10942,#10943,#10944));
#2686=EDGE_LOOP('',(#10945));
#2687=EDGE_LOOP('',(#10946));
#2688=EDGE_LOOP('',(#10947,#10948,#10949,#10950));
#2689=EDGE_LOOP('',(#10951,#10952,#10953,#10954));
#2690=EDGE_LOOP('',(#10955,#10956,#10957,#10958));
#2691=EDGE_LOOP('',(#10959,#10960,#10961,#10962,#10963,#10964,#10965,#10966,
#10967,#10968,#10969,#10970));
#2692=EDGE_LOOP('',(#10971));
#2693=EDGE_LOOP('',(#10972));
#2694=EDGE_LOOP('',(#10973,#10974,#10975,#10976));
#2695=EDGE_LOOP('',(#10977,#10978,#10979,#10980));
#2696=EDGE_LOOP('',(#10981,#10982,#10983,#10984));
#2697=EDGE_LOOP('',(#10985,#10986,#10987,#10988,#10989,#10990,#10991,#10992,
#10993,#10994,#10995,#10996));
#2698=EDGE_LOOP('',(#10997));
#2699=EDGE_LOOP('',(#10998));
#2700=EDGE_LOOP('',(#10999,#11000,#11001,#11002));
#2701=EDGE_LOOP('',(#11003,#11004,#11005,#11006));
#2702=EDGE_LOOP('',(#11007,#11008,#11009,#11010));
#2703=EDGE_LOOP('',(#11011,#11012,#11013,#11014,#11015,#11016,#11017,#11018,
#11019,#11020,#11021,#11022));
#2704=EDGE_LOOP('',(#11023));
#2705=EDGE_LOOP('',(#11024));
#2706=EDGE_LOOP('',(#11025,#11026,#11027,#11028));
#2707=EDGE_LOOP('',(#11029,#11030,#11031,#11032));
#2708=EDGE_LOOP('',(#11033,#11034,#11035,#11036));
#2709=EDGE_LOOP('',(#11037,#11038,#11039,#11040,#11041,#11042,#11043,#11044,
#11045,#11046,#11047,#11048));
#2710=EDGE_LOOP('',(#11049));
#2711=EDGE_LOOP('',(#11050));
#2712=EDGE_LOOP('',(#11051,#11052,#11053,#11054));
#2713=EDGE_LOOP('',(#11055,#11056,#11057,#11058));
#2714=EDGE_LOOP('',(#11059,#11060,#11061,#11062));
#2715=EDGE_LOOP('',(#11063,#11064,#11065,#11066,#11067,#11068,#11069,#11070,
#11071,#11072,#11073,#11074));
#2716=EDGE_LOOP('',(#11075));
#2717=EDGE_LOOP('',(#11076));
#2718=EDGE_LOOP('',(#11077,#11078,#11079,#11080,#11081,#11082,#11083,#11084,
#11085,#11086,#11087,#11088));
#2719=EDGE_LOOP('',(#11089));
#2720=EDGE_LOOP('',(#11090));
#2721=EDGE_LOOP('',(#11091,#11092,#11093,#11094));
#2722=EDGE_LOOP('',(#11095,#11096,#11097,#11098));
#2723=EDGE_LOOP('',(#11099,#11100,#11101,#11102));
#2724=EDGE_LOOP('',(#11103,#11104,#11105,#11106));
#2725=EDGE_LOOP('',(#11107,#11108,#11109,#11110));
#2726=EDGE_LOOP('',(#11111,#11112,#11113,#11114));
#2727=EDGE_LOOP('',(#11115,#11116,#11117,#11118));
#2728=EDGE_LOOP('',(#11119));
#2729=EDGE_LOOP('',(#11120));
#2730=EDGE_LOOP('',(#11121));
#2731=EDGE_LOOP('',(#11122));
#2732=EDGE_LOOP('',(#11123,#11124,#11125,#11126));
#2733=EDGE_LOOP('',(#11127,#11128,#11129,#11130,#11131,#11132));
#2734=EDGE_LOOP('',(#11133,#11134,#11135,#11136));
#2735=EDGE_LOOP('',(#11137,#11138,#11139,#11140));
#2736=EDGE_LOOP('',(#11141));
#2737=EDGE_LOOP('',(#11142));
#2738=EDGE_LOOP('',(#11143));
#2739=EDGE_LOOP('',(#11144));
#2740=EDGE_LOOP('',(#11145,#11146,#11147,#11148));
#2741=EDGE_LOOP('',(#11149,#11150,#11151,#11152));
#2742=EDGE_LOOP('',(#11153,#11154,#11155,#11156));
#2743=EDGE_LOOP('',(#11157,#11158,#11159,#11160));
#2744=EDGE_LOOP('',(#11161,#11162,#11163,#11164));
#2745=EDGE_LOOP('',(#11165,#11166,#11167,#11168));
#2746=EDGE_LOOP('',(#11169,#11170,#11171,#11172,#11173,#11174));
#2747=EDGE_LOOP('',(#11175,#11176,#11177,#11178));
#2748=EDGE_LOOP('',(#11179));
#2749=EDGE_LOOP('',(#11180));
#2750=EDGE_LOOP('',(#11181));
#2751=EDGE_LOOP('',(#11182));
#2752=EDGE_LOOP('',(#11183,#11184,#11185,#11186));
#2753=EDGE_LOOP('',(#11187,#11188,#11189,#11190));
#2754=EDGE_LOOP('',(#11191,#11192,#11193,#11194));
#2755=EDGE_LOOP('',(#11195,#11196,#11197,#11198));
#2756=EDGE_LOOP('',(#11199,#11200,#11201,#11202));
#2757=EDGE_LOOP('',(#11203,#11204,#11205,#11206));
#2758=EDGE_LOOP('',(#11207,#11208,#11209,#11210,#11211,#11212));
#2759=EDGE_LOOP('',(#11213,#11214,#11215,#11216));
#2760=EDGE_LOOP('',(#11217));
#2761=EDGE_LOOP('',(#11218));
#2762=EDGE_LOOP('',(#11219));
#2763=EDGE_LOOP('',(#11220));
#2764=EDGE_LOOP('',(#11221,#11222,#11223,#11224));
#2765=EDGE_LOOP('',(#11225,#11226,#11227,#11228));
#2766=EDGE_LOOP('',(#11229,#11230,#11231,#11232));
#2767=EDGE_LOOP('',(#11233,#11234,#11235,#11236));
#2768=EDGE_LOOP('',(#11237,#11238,#11239,#11240));
#2769=EDGE_LOOP('',(#11241,#11242,#11243,#11244));
#2770=EDGE_LOOP('',(#11245,#11246,#11247,#11248,#11249,#11250));
#2771=EDGE_LOOP('',(#11251,#11252,#11253,#11254));
#2772=EDGE_LOOP('',(#11255));
#2773=EDGE_LOOP('',(#11256));
#2774=EDGE_LOOP('',(#11257));
#2775=EDGE_LOOP('',(#11258));
#2776=EDGE_LOOP('',(#11259,#11260,#11261,#11262));
#2777=EDGE_LOOP('',(#11263,#11264,#11265,#11266));
#2778=EDGE_LOOP('',(#11267,#11268,#11269,#11270));
#2779=EDGE_LOOP('',(#11271,#11272,#11273,#11274));
#2780=EDGE_LOOP('',(#11275,#11276,#11277,#11278));
#2781=EDGE_LOOP('',(#11279,#11280,#11281,#11282));
#2782=EDGE_LOOP('',(#11283,#11284,#11285,#11286,#11287,#11288));
#2783=EDGE_LOOP('',(#11289,#11290,#11291,#11292));
#2784=EDGE_LOOP('',(#11293));
#2785=EDGE_LOOP('',(#11294));
#2786=EDGE_LOOP('',(#11295));
#2787=EDGE_LOOP('',(#11296));
#2788=EDGE_LOOP('',(#11297,#11298,#11299,#11300));
#2789=EDGE_LOOP('',(#11301,#11302,#11303,#11304));
#2790=EDGE_LOOP('',(#11305,#11306,#11307,#11308));
#2791=EDGE_LOOP('',(#11309,#11310,#11311,#11312));
#2792=EDGE_LOOP('',(#11313,#11314,#11315,#11316));
#2793=EDGE_LOOP('',(#11317,#11318,#11319,#11320));
#2794=EDGE_LOOP('',(#11321,#11322,#11323,#11324,#11325,#11326));
#2795=EDGE_LOOP('',(#11327,#11328,#11329,#11330));
#2796=EDGE_LOOP('',(#11331));
#2797=EDGE_LOOP('',(#11332));
#2798=EDGE_LOOP('',(#11333));
#2799=EDGE_LOOP('',(#11334));
#2800=EDGE_LOOP('',(#11335,#11336,#11337,#11338));
#2801=EDGE_LOOP('',(#11339,#11340,#11341,#11342));
#2802=EDGE_LOOP('',(#11343,#11344,#11345,#11346));
#2803=EDGE_LOOP('',(#11347,#11348,#11349,#11350));
#2804=EDGE_LOOP('',(#11351,#11352,#11353,#11354));
#2805=EDGE_LOOP('',(#11355,#11356,#11357,#11358,#11359,#11360));
#2806=EDGE_LOOP('',(#11361,#11362,#11363,#11364));
#2807=EDGE_LOOP('',(#11365,#11366,#11367,#11368));
#3395=LINE('',#40877,#3843);
#3396=LINE('',#40880,#3844);
#3397=LINE('',#40883,#3845);
#3398=LINE('',#40888,#3846);
#3399=LINE('',#40891,#3847);
#3400=LINE('',#40955,#3848);
#3401=LINE('',#40959,#3849);
#3402=LINE('',#40964,#3850);
#3403=LINE('',#40970,#3851);
#3404=LINE('',#40974,#3852);
#3405=LINE('',#40979,#3853);
#3406=LINE('',#40985,#3854);
#3407=LINE('',#40993,#3855);
#3408=LINE('',#40996,#3856);
#3843=VECTOR('',#17477,8.14999999999999);
#3844=VECTOR('',#17482,7.5);
#3845=VECTOR('',#17485,7.5);
#3846=VECTOR('',#17492,12.4653846153846);
#3847=VECTOR('',#17495,12.4653846153846);
#3848=VECTOR('',#17570,17.6897435897436);
#3849=VECTOR('',#17575,16.2686153846154);
#3850=VECTOR('',#17582,16.0346153846154);
#3851=VECTOR('',#17591,16.0346153846154);
#3852=VECTOR('',#17596,16.2686153846154);
#3853=VECTOR('',#17601,17.6897435897436);
#3854=VECTOR('',#17608,20.35);
#3855=VECTOR('',#17617,21.);
#3856=VECTOR('',#17622,21.);
#4529=CIRCLE('',#14255,12.4653846153846);
#4530=CIRCLE('',#14256,3.56616156686793);
#4531=CIRCLE('',#14257,12.4653846153846);
#4532=CIRCLE('',#14259,7.64278544417155);
#4533=CIRCLE('',#14260,0.4875);
#4534=CIRCLE('',#14261,7.5);
#4535=CIRCLE('',#14262,7.5);
#4536=CIRCLE('',#14263,7.64278544417155);
#4537=CIRCLE('',#14265,7.5);
#4538=CIRCLE('',#14266,0.4875);
#4539=CIRCLE('',#14267,7.64278544417155);
#4540=CIRCLE('',#14268,7.5);
#4541=CIRCLE('',#14270,8.14999999999999);
#4542=CIRCLE('',#14273,8.14999999999999);
#4543=CIRCLE('',#14275,12.4653846153846);
#4544=CIRCLE('',#14277,12.4653846153846);
#4545=CIRCLE('',#14281,3.56616156686793);
#4546=CIRCLE('',#14283,3.56616156686793);
#4547=CIRCLE('',#14285,3.56616156686793);
#4548=CIRCLE('',#14287,3.56616156686793);
#4549=CIRCLE('',#14289,3.56616156686793);
#4550=CIRCLE('',#14291,3.56616156686793);
#4551=CIRCLE('',#14293,3.56616156686793);
#4552=CIRCLE('',#14295,16.3271153846154);
#4553=CIRCLE('',#14296,0.0585);
#4554=CIRCLE('',#14297,16.2686153846154);
#4555=CIRCLE('',#14298,16.2686153846154);
#4556=CIRCLE('',#14300,16.0346153846154);
#4557=CIRCLE('',#14301,0.0585);
#4558=CIRCLE('',#14302,16.0931153846154);
#4559=CIRCLE('',#14304,16.3271153846154);
#4560=CIRCLE('',#14305,0.0585);
#4561=CIRCLE('',#14306,16.2686153846154);
#4562=CIRCLE('',#14308,16.0346153846154);
#4563=CIRCLE('',#14309,0.0585);
#4564=CIRCLE('',#14310,16.0931153846154);
#4565=CIRCLE('',#14311,16.0346153846154);
#4566=CIRCLE('',#14313,17.6897435897436);
#4567=CIRCLE('',#14314,17.6897435897436);
#4568=CIRCLE('',#14316,16.2686153846154);
#4569=CIRCLE('',#14318,16.0346153846154);
#4570=CIRCLE('',#14320,3.56616156686793);
#4571=CIRCLE('',#14321,16.0346153846154);
#4572=CIRCLE('',#14324,16.2686153846154);
#4573=CIRCLE('',#14326,17.6897435897436);
#4574=CIRCLE('',#14327,17.6897435897436);
#4575=CIRCLE('',#14329,21.);
#4576=CIRCLE('',#14330,20.35);
#4577=CIRCLE('',#14332,21.);
#4578=CIRCLE('',#14333,21.);
#4579=CIRCLE('',#14334,20.35);
#4580=CIRCLE('',#14343,3.96060240207311);
#4581=CIRCLE('',#14344,1.69469015025);
#4582=CIRCLE('',#14345,3.96060240207311);
#4583=CIRCLE('',#14347,3.39763111739558);
#4584=CIRCLE('',#14348,3.39763111739558);
#4585=CIRCLE('',#14349,3.39763111739558);
#4586=CIRCLE('',#14350,3.56616156686792);
#4587=CIRCLE('',#14351,3.39763111739558);
#4588=CIRCLE('',#14352,3.39763111739558);
#4589=CIRCLE('',#14353,3.39763111739558);
#4590=CIRCLE('',#14354,3.45272288248773);
#4591=CIRCLE('',#14355,3.45272288248773);
#4592=CIRCLE('',#14357,3.96060240207311);
#4593=CIRCLE('',#14358,1.69469015025);
#4594=CIRCLE('',#14359,3.96060240207311);
#4595=CIRCLE('',#14361,3.39763111739558);
#4596=CIRCLE('',#14362,3.39763111739558);
#4597=CIRCLE('',#14363,3.39763111739558);
#4598=CIRCLE('',#14364,3.56616156686792);
#4599=CIRCLE('',#14365,3.39763111739558);
#4600=CIRCLE('',#14366,3.39763111739558);
#4601=CIRCLE('',#14367,3.39763111739558);
#4602=CIRCLE('',#14368,3.45272288248773);
#4603=CIRCLE('',#14369,3.45272288248773);
#4604=CIRCLE('',#14371,3.96060240207311);
#4605=CIRCLE('',#14372,1.69469015025);
#4606=CIRCLE('',#14373,3.96060240207311);
#4607=CIRCLE('',#14375,3.39763111739558);
#4608=CIRCLE('',#14376,3.39763111739558);
#4609=CIRCLE('',#14377,3.39763111739558);
#4610=CIRCLE('',#14378,3.56616156686792);
#4611=CIRCLE('',#14379,3.39763111739558);
#4612=CIRCLE('',#14380,3.39763111739558);
#4613=CIRCLE('',#14381,3.39763111739558);
#4614=CIRCLE('',#14382,3.45272288248773);
#4615=CIRCLE('',#14383,3.45272288248773);
#4616=CIRCLE('',#14385,3.96060240207311);
#4617=CIRCLE('',#14386,1.69469015025);
#4618=CIRCLE('',#14387,3.96060240207311);
#4619=CIRCLE('',#14389,3.39763111739558);
#4620=CIRCLE('',#14390,3.39763111739558);
#4621=CIRCLE('',#14391,3.39763111739558);
#4622=CIRCLE('',#14392,3.56616156686792);
#4623=CIRCLE('',#14393,3.39763111739558);
#4624=CIRCLE('',#14394,3.39763111739558);
#4625=CIRCLE('',#14395,3.39763111739558);
#4626=CIRCLE('',#14396,3.45272288248773);
#4627=CIRCLE('',#14397,3.45272288248773);
#4628=CIRCLE('',#14399,3.96060240207311);
#4629=CIRCLE('',#14400,1.69469015025);
#4630=CIRCLE('',#14401,3.96060240207311);
#4631=CIRCLE('',#14403,3.39763111739558);
#4632=CIRCLE('',#14404,3.39763111739558);
#4633=CIRCLE('',#14405,3.39763111739558);
#4634=CIRCLE('',#14406,3.56616156686792);
#4635=CIRCLE('',#14407,3.39763111739558);
#4636=CIRCLE('',#14408,3.39763111739558);
#4637=CIRCLE('',#14409,3.39763111739558);
#4638=CIRCLE('',#14410,3.45272288248773);
#4639=CIRCLE('',#14411,3.45272288248773);
#4640=CIRCLE('',#14413,3.96060240207311);
#4641=CIRCLE('',#14414,1.69469015025);
#4642=CIRCLE('',#14415,3.96060240207311);
#4643=CIRCLE('',#14417,3.39763111739558);
#4644=CIRCLE('',#14418,3.56616156686792);
#4645=CIRCLE('',#14419,3.39763111739558);
#4646=CIRCLE('',#14420,3.39763111739558);
#4647=CIRCLE('',#14421,3.39763111739558);
#4648=CIRCLE('',#14422,3.39763111739558);
#4649=CIRCLE('',#14423,3.39763111739558);
#4650=CIRCLE('',#14424,3.45272288248773);
#4651=CIRCLE('',#14425,3.45272288248773);
#4652=CIRCLE('',#14427,3.39763111739558);
#4653=CIRCLE('',#14428,3.39763111739558);
#4654=CIRCLE('',#14429,3.39763111739558);
#4655=CIRCLE('',#14430,3.56616156686792);
#4656=CIRCLE('',#14431,3.39763111739558);
#4657=CIRCLE('',#14432,3.39763111739558);
#4658=CIRCLE('',#14433,3.39763111739558);
#4659=CIRCLE('',#14434,3.45272288248773);
#4660=CIRCLE('',#14435,3.45272288248773);
#4661=CIRCLE('',#14437,3.96060240207311);
#4662=CIRCLE('',#14438,1.69469015025);
#4663=CIRCLE('',#14439,3.96060240207311);
#4664=CIRCLE('',#14441,14.25);
#4665=CIRCLE('',#14442,14.25);
#4666=CIRCLE('',#14444,15.1423076923077);
#4667=CIRCLE('',#14445,15.1423076923077);
#4668=CIRCLE('',#14451,14.25);
#4669=CIRCLE('',#14452,15.1423076923077);
#4670=CIRCLE('',#14454,15.1423076923077);
#4671=CIRCLE('',#14455,14.25);
#4672=CIRCLE('',#14461,15.1423076923077);
#4673=CIRCLE('',#14462,14.25);
#4674=CIRCLE('',#14464,14.25);
#4675=CIRCLE('',#14465,15.1423076923077);
#4676=CIRCLE('',#14469,14.25);
#4677=CIRCLE('',#14470,14.25);
#4678=CIRCLE('',#14472,15.1423076923077);
#4679=CIRCLE('',#14473,15.1423076923077);
#4680=CIRCLE('',#14479,15.1423076923077);
#4681=CIRCLE('',#14480,14.25);
#4682=CIRCLE('',#14482,14.25);
#4683=CIRCLE('',#14483,15.1423076923077);
#4684=CIRCLE('',#14487,14.25);
#4685=CIRCLE('',#14488,14.25);
#4686=CIRCLE('',#14490,15.1423076923077);
#4687=CIRCLE('',#14491,15.1423076923077);
#4688=CIRCLE('',#14497,15.1423076923077);
#4689=CIRCLE('',#14498,14.25);
#4690=CIRCLE('',#14500,14.25);
#4691=CIRCLE('',#14501,15.1423076923077);
#4692=CIRCLE('',#14505,14.25);
#4693=CIRCLE('',#14506,14.25);
#4694=CIRCLE('',#14508,15.1423076923077);
#4695=CIRCLE('',#14509,15.1423076923077);
#4696=CIRCLE('',#14515,15.1423076923077);
#4697=CIRCLE('',#14516,14.25);
#4698=CIRCLE('',#14518,14.25);
#4699=CIRCLE('',#14519,15.1423076923077);
#4700=CIRCLE('',#14523,14.25);
#4701=CIRCLE('',#14524,14.25);
#4702=CIRCLE('',#14526,15.1423076923077);
#4703=CIRCLE('',#14527,15.1423076923077);
#4704=CIRCLE('',#14533,15.1423076923077);
#4705=CIRCLE('',#14534,14.25);
#4706=CIRCLE('',#14536,14.25);
#4707=CIRCLE('',#14537,15.1423076923077);
#4708=CIRCLE('',#14541,14.25);
#4709=CIRCLE('',#14542,14.25);
#4710=CIRCLE('',#14544,15.1423076923077);
#4711=CIRCLE('',#14545,15.1423076923077);
#4712=CIRCLE('',#14551,15.1423076923077);
#4713=CIRCLE('',#14552,14.25);
#4714=CIRCLE('',#14554,14.25);
#4715=CIRCLE('',#14555,15.1423076923077);
#4716=CIRCLE('',#14559,15.1423076923077);
#4717=CIRCLE('',#14560,14.25);
#4718=CIRCLE('',#14562,14.25);
#4719=CIRCLE('',#14563,15.1423076923077);
#5815=VERTEX_POINT('',#40852);
#5816=VERTEX_POINT('',#40854);
#5817=VERTEX_POINT('',#40858);
#5818=VERTEX_POINT('',#40859);
#5819=VERTEX_POINT('',#40861);
#5820=VERTEX_POINT('',#40863);
#5821=VERTEX_POINT('',#40868);
#5822=VERTEX_POINT('',#40869);
#5823=VERTEX_POINT('',#40871);
#5824=VERTEX_POINT('',#40876);
#5825=VERTEX_POINT('',#40882);
#5826=VERTEX_POINT('',#40886);
#5827=VERTEX_POINT('',#40890);
#5828=VERTEX_POINT('',#40896);
#5829=VERTEX_POINT('',#40897);
#5830=VERTEX_POINT('',#40900);
#5831=VERTEX_POINT('',#40901);
#5832=VERTEX_POINT('',#40904);
#5833=VERTEX_POINT('',#40905);
#5834=VERTEX_POINT('',#40908);
#5835=VERTEX_POINT('',#40909);
#5836=VERTEX_POINT('',#40912);
#5837=VERTEX_POINT('',#40913);
#5838=VERTEX_POINT('',#40916);
#5839=VERTEX_POINT('',#40917);
#5840=VERTEX_POINT('',#40920);
#5841=VERTEX_POINT('',#40921);
#5842=VERTEX_POINT('',#40924);
#5843=VERTEX_POINT('',#40926);
#5844=VERTEX_POINT('',#40928);
#5845=VERTEX_POINT('',#40932);
#5846=VERTEX_POINT('',#40934);
#5847=VERTEX_POINT('',#40938);
#5848=VERTEX_POINT('',#40940);
#5849=VERTEX_POINT('',#40944);
#5850=VERTEX_POINT('',#40945);
#5851=VERTEX_POINT('',#40947);
#5852=VERTEX_POINT('',#40952);
#5853=VERTEX_POINT('',#40954);
#5854=VERTEX_POINT('',#40958);
#5855=VERTEX_POINT('',#40962);
#5856=VERTEX_POINT('',#40966);
#5857=VERTEX_POINT('',#40972);
#5858=VERTEX_POINT('',#40976);
#5859=VERTEX_POINT('',#40978);
#5860=VERTEX_POINT('',#40982);
#5861=VERTEX_POINT('',#40984);
#5862=VERTEX_POINT('',#40988);
#5863=VERTEX_POINT('',#40989);
#5864=VERTEX_POINT('',#40992);
#5865=VERTEX_POINT('',#41004);
#5866=VERTEX_POINT('',#41006);
#5867=VERTEX_POINT('',#41009);
#5868=VERTEX_POINT('',#41010);
#5869=VERTEX_POINT('',#41017);
#5870=VERTEX_POINT('',#41037);
#5871=VERTEX_POINT('',#41063);
#5872=VERTEX_POINT('',#41064);
#5873=VERTEX_POINT('',#41071);
#5874=VERTEX_POINT('',#41091);
#5875=VERTEX_POINT('',#41118);
#5876=VERTEX_POINT('',#41119);
#5877=VERTEX_POINT('',#41121);
#5878=VERTEX_POINT('',#41128);
#5879=VERTEX_POINT('',#41130);
#5880=VERTEX_POINT('',#41138);
#5881=VERTEX_POINT('',#41140);
#5882=VERTEX_POINT('',#41142);
#5883=VERTEX_POINT('',#41150);
#5884=VERTEX_POINT('',#41152);
#5885=VERTEX_POINT('',#41161);
#5886=VERTEX_POINT('',#41163);
#5887=VERTEX_POINT('',#41166);
#5888=VERTEX_POINT('',#41168);
#5889=VERTEX_POINT('',#41171);
#5890=VERTEX_POINT('',#41172);
#5891=VERTEX_POINT('',#41179);
#5892=VERTEX_POINT('',#41199);
#5893=VERTEX_POINT('',#41225);
#5894=VERTEX_POINT('',#41226);
#5895=VERTEX_POINT('',#41233);
#5896=VERTEX_POINT('',#41253);
#5897=VERTEX_POINT('',#41280);
#5898=VERTEX_POINT('',#41281);
#5899=VERTEX_POINT('',#41283);
#5900=VERTEX_POINT('',#41290);
#5901=VERTEX_POINT('',#41292);
#5902=VERTEX_POINT('',#41300);
#5903=VERTEX_POINT('',#41302);
#5904=VERTEX_POINT('',#41304);
#5905=VERTEX_POINT('',#41312);
#5906=VERTEX_POINT('',#41314);
#5907=VERTEX_POINT('',#41323);
#5908=VERTEX_POINT('',#41325);
#5909=VERTEX_POINT('',#41328);
#5910=VERTEX_POINT('',#41330);
#5911=VERTEX_POINT('',#41333);
#5912=VERTEX_POINT('',#41334);
#5913=VERTEX_POINT('',#41341);
#5914=VERTEX_POINT('',#41361);
#5915=VERTEX_POINT('',#41387);
#5916=VERTEX_POINT('',#41388);
#5917=VERTEX_POINT('',#41395);
#5918=VERTEX_POINT('',#41415);
#5919=VERTEX_POINT('',#41442);
#5920=VERTEX_POINT('',#41443);
#5921=VERTEX_POINT('',#41445);
#5922=VERTEX_POINT('',#41452);
#5923=VERTEX_POINT('',#41454);
#5924=VERTEX_POINT('',#41462);
#5925=VERTEX_POINT('',#41464);
#5926=VERTEX_POINT('',#41466);
#5927=VERTEX_POINT('',#41474);
#5928=VERTEX_POINT('',#41476);
#5929=VERTEX_POINT('',#41485);
#5930=VERTEX_POINT('',#41487);
#5931=VERTEX_POINT('',#41490);
#5932=VERTEX_POINT('',#41492);
#5933=VERTEX_POINT('',#41495);
#5934=VERTEX_POINT('',#41496);
#5935=VERTEX_POINT('',#41503);
#5936=VERTEX_POINT('',#41523);
#5937=VERTEX_POINT('',#41549);
#5938=VERTEX_POINT('',#41550);
#5939=VERTEX_POINT('',#41557);
#5940=VERTEX_POINT('',#41577);
#5941=VERTEX_POINT('',#41604);
#5942=VERTEX_POINT('',#41605);
#5943=VERTEX_POINT('',#41607);
#5944=VERTEX_POINT('',#41614);
#5945=VERTEX_POINT('',#41616);
#5946=VERTEX_POINT('',#41624);
#5947=VERTEX_POINT('',#41626);
#5948=VERTEX_POINT('',#41628);
#5949=VERTEX_POINT('',#41636);
#5950=VERTEX_POINT('',#41638);
#5951=VERTEX_POINT('',#41647);
#5952=VERTEX_POINT('',#41649);
#5953=VERTEX_POINT('',#41652);
#5954=VERTEX_POINT('',#41654);
#5955=VERTEX_POINT('',#41657);
#5956=VERTEX_POINT('',#41658);
#5957=VERTEX_POINT('',#41665);
#5958=VERTEX_POINT('',#41685);
#5959=VERTEX_POINT('',#41711);
#5960=VERTEX_POINT('',#41712);
#5961=VERTEX_POINT('',#41719);
#5962=VERTEX_POINT('',#41739);
#5963=VERTEX_POINT('',#41766);
#5964=VERTEX_POINT('',#41767);
#5965=VERTEX_POINT('',#41769);
#5966=VERTEX_POINT('',#41776);
#5967=VERTEX_POINT('',#41778);
#5968=VERTEX_POINT('',#41786);
#5969=VERTEX_POINT('',#41788);
#5970=VERTEX_POINT('',#41790);
#5971=VERTEX_POINT('',#41798);
#5972=VERTEX_POINT('',#41800);
#5973=VERTEX_POINT('',#41809);
#5974=VERTEX_POINT('',#41811);
#5975=VERTEX_POINT('',#41814);
#5976=VERTEX_POINT('',#41816);
#5977=VERTEX_POINT('',#41819);
#5978=VERTEX_POINT('',#41820);
#5979=VERTEX_POINT('',#41840);
#5980=VERTEX_POINT('',#41847);
#5981=VERTEX_POINT('',#41873);
#5982=VERTEX_POINT('',#41874);
#5983=VERTEX_POINT('',#41881);
#5984=VERTEX_POINT('',#41901);
#5985=VERTEX_POINT('',#41928);
#5986=VERTEX_POINT('',#41929);
#5987=VERTEX_POINT('',#41931);
#5988=VERTEX_POINT('',#41933);
#5989=VERTEX_POINT('',#41935);
#5990=VERTEX_POINT('',#41943);
#5991=VERTEX_POINT('',#41945);
#5992=VERTEX_POINT('',#41954);
#5993=VERTEX_POINT('',#41956);
#5994=VERTEX_POINT('',#41963);
#5995=VERTEX_POINT('',#41971);
#5996=VERTEX_POINT('',#41973);
#5997=VERTEX_POINT('',#41976);
#5998=VERTEX_POINT('',#41977);
#5999=VERTEX_POINT('',#41979);
#6000=VERTEX_POINT('',#41986);
#6001=VERTEX_POINT('',#41988);
#6002=VERTEX_POINT('',#41996);
#6003=VERTEX_POINT('',#41998);
#6004=VERTEX_POINT('',#42000);
#6005=VERTEX_POINT('',#42008);
#6006=VERTEX_POINT('',#42010);
#6007=VERTEX_POINT('',#42019);
#6008=VERTEX_POINT('',#42021);
#6009=VERTEX_POINT('',#42024);
#6010=VERTEX_POINT('',#42026);
#6011=VERTEX_POINT('',#42029);
#6012=VERTEX_POINT('',#42030);
#6013=VERTEX_POINT('',#42037);
#6014=VERTEX_POINT('',#42057);
#6015=VERTEX_POINT('',#42083);
#6016=VERTEX_POINT('',#42084);
#6017=VERTEX_POINT('',#42091);
#6018=VERTEX_POINT('',#42111);
#7557=EDGE_CURVE('',#5815,#5815,#4529,.T.);
#7558=EDGE_CURVE('',#5815,#5816,#4530,.T.);
#7559=EDGE_CURVE('',#5816,#5816,#4531,.T.);
#7560=EDGE_CURVE('',#5817,#5818,#4532,.T.);
#7561=EDGE_CURVE('',#5818,#5819,#4533,.T.);
#7562=EDGE_CURVE('',#5819,#5820,#4534,.T.);
#7563=EDGE_CURVE('',#5820,#5819,#4535,.T.);
#7564=EDGE_CURVE('',#5818,#5817,#4536,.T.);
#7565=EDGE_CURVE('',#5821,#5822,#4537,.T.);
#7566=EDGE_CURVE('',#5822,#5823,#4538,.T.);
#7567=EDGE_CURVE('',#5823,#5823,#4539,.T.);
#7568=EDGE_CURVE('',#5822,#5821,#4540,.T.);
#7569=EDGE_CURVE('',#5817,#5824,#3395,.T.);
#7570=EDGE_CURVE('',#5824,#5824,#4541,.T.);
#7571=EDGE_CURVE('',#5820,#5821,#3396,.T.);
#7572=EDGE_CURVE('',#5823,#5825,#3397,.T.);
#7573=EDGE_CURVE('',#5825,#5825,#4542,.T.);
#7574=EDGE_CURVE('',#5826,#5826,#4543,.T.);
#7575=EDGE_CURVE('',#5826,#5816,#3398,.T.);
#7576=EDGE_CURVE('',#5815,#5827,#3399,.T.);
#7577=EDGE_CURVE('',#5827,#5827,#4544,.T.);
#7578=EDGE_CURVE('',#5828,#5829,#4545,.T.);
#7579=EDGE_CURVE('',#5830,#5831,#4546,.T.);
#7580=EDGE_CURVE('',#5832,#5833,#4547,.T.);
#7581=EDGE_CURVE('',#5834,#5835,#4548,.T.);
#7582=EDGE_CURVE('',#5836,#5837,#4549,.T.);
#7583=EDGE_CURVE('',#5838,#5839,#4550,.T.);
#7584=EDGE_CURVE('',#5840,#5841,#4551,.T.);
#7585=EDGE_CURVE('',#5842,#5842,#4552,.T.);
#7586=EDGE_CURVE('',#5842,#5843,#4553,.T.);
#7587=EDGE_CURVE('',#5843,#5844,#4554,.T.);
#7588=EDGE_CURVE('',#5844,#5843,#4555,.T.);
#7589=EDGE_CURVE('',#5845,#5845,#4556,.T.);
#7590=EDGE_CURVE('',#5845,#5846,#4557,.T.);
#7591=EDGE_CURVE('',#5846,#5846,#4558,.T.);
#7592=EDGE_CURVE('',#5847,#5847,#4559,.T.);
#7593=EDGE_CURVE('',#5847,#5848,#4560,.T.);
#7594=EDGE_CURVE('',#5848,#5848,#4561,.T.);
#7595=EDGE_CURVE('',#5849,#5850,#4562,.T.);
#7596=EDGE_CURVE('',#5850,#5851,#4563,.T.);
#7597=EDGE_CURVE('',#5851,#5851,#4564,.T.);
#7598=EDGE_CURVE('',#5850,#5849,#4565,.T.);
#7599=EDGE_CURVE('',#5852,#5852,#4566,.T.);
#7600=EDGE_CURVE('',#5852,#5853,#3400,.T.);
#7601=EDGE_CURVE('',#5853,#5853,#4567,.T.);
#7602=EDGE_CURVE('',#5844,#5854,#3401,.T.);
#7603=EDGE_CURVE('',#5854,#5854,#4568,.T.);
#7604=EDGE_CURVE('',#5855,#5855,#4569,.T.);
#7605=EDGE_CURVE('',#5855,#5849,#3402,.T.);
#7606=EDGE_CURVE('',#5855,#5856,#4570,.T.);
#7607=EDGE_CURVE('',#5856,#5856,#4571,.T.);
#7608=EDGE_CURVE('',#5845,#5856,#3403,.T.);
#7609=EDGE_CURVE('',#5857,#5857,#4572,.T.);
#7610=EDGE_CURVE('',#5857,#5848,#3404,.T.);
#7611=EDGE_CURVE('',#5858,#5858,#4573,.T.);
#7612=EDGE_CURVE('',#5858,#5859,#3405,.T.);
#7613=EDGE_CURVE('',#5859,#5859,#4574,.T.);
#7614=EDGE_CURVE('',#5860,#5860,#4575,.T.);
#7615=EDGE_CURVE('',#5860,#5861,#3406,.T.);
#7616=EDGE_CURVE('',#5861,#5861,#4576,.T.);
#7617=EDGE_CURVE('',#5862,#5863,#4577,.T.);
#7618=EDGE_CURVE('',#5863,#5862,#4578,.T.);
#7619=EDGE_CURVE('',#5863,#5864,#3407,.T.);
#7620=EDGE_CURVE('',#5864,#5864,#4579,.T.);
#7621=EDGE_CURVE('',#5860,#5862,#3408,.T.);
#7622=EDGE_CURVE('',#5865,#5865,#4580,.T.);
#7623=EDGE_CURVE('',#5865,#5866,#4581,.T.);
#7624=EDGE_CURVE('',#5866,#5866,#4582,.T.);
#7625=EDGE_CURVE('',#5867,#5868,#779,.T.);
#7626=EDGE_CURVE('',#5869,#5868,#780,.T.);
#7627=EDGE_CURVE('',#5870,#5869,#781,.T.);
#7628=EDGE_CURVE('',#5867,#5870,#782,.T.);
#7629=EDGE_CURVE('',#5871,#5872,#783,.T.);
#7630=EDGE_CURVE('',#5873,#5872,#784,.T.);
#7631=EDGE_CURVE('',#5874,#5873,#785,.T.);
#7632=EDGE_CURVE('',#5871,#5874,#786,.T.);
#7633=EDGE_CURVE('',#5875,#5876,#4583,.T.);
#7634=EDGE_CURVE('',#5877,#5875,#787,.T.);
#7635=EDGE_CURVE('',#5877,#5878,#4584,.T.);
#7636=EDGE_CURVE('',#5879,#5878,#788,.T.);
#7637=EDGE_CURVE('',#5876,#5879,#4585,.T.);
#7638=EDGE_CURVE('',#5876,#5880,#4586,.T.);
#7639=EDGE_CURVE('',#5881,#5880,#4587,.T.);
#7640=EDGE_CURVE('',#5882,#5881,#789,.T.);
#7641=EDGE_CURVE('',#5882,#5883,#4588,.T.);
#7642=EDGE_CURVE('',#5884,#5883,#790,.T.);
#7643=EDGE_CURVE('',#5880,#5884,#4589,.T.);
#7644=EDGE_CURVE('',#5885,#5885,#4590,.T.);
#7645=EDGE_CURVE('',#5886,#5886,#4591,.T.);
#7646=EDGE_CURVE('',#5887,#5887,#4592,.T.);
#7647=EDGE_CURVE('',#5887,#5888,#4593,.T.);
#7648=EDGE_CURVE('',#5888,#5888,#4594,.T.);
#7649=EDGE_CURVE('',#5889,#5890,#791,.T.);
#7650=EDGE_CURVE('',#5891,#5890,#792,.T.);
#7651=EDGE_CURVE('',#5892,#5891,#793,.T.);
#7652=EDGE_CURVE('',#5889,#5892,#794,.T.);
#7653=EDGE_CURVE('',#5893,#5894,#795,.T.);
#7654=EDGE_CURVE('',#5895,#5894,#796,.T.);
#7655=EDGE_CURVE('',#5896,#5895,#797,.T.);
#7656=EDGE_CURVE('',#5893,#5896,#798,.T.);
#7657=EDGE_CURVE('',#5897,#5898,#4595,.T.);
#7658=EDGE_CURVE('',#5899,#5897,#799,.T.);
#7659=EDGE_CURVE('',#5899,#5900,#4596,.T.);
#7660=EDGE_CURVE('',#5901,#5900,#800,.T.);
#7661=EDGE_CURVE('',#5898,#5901,#4597,.T.);
#7662=EDGE_CURVE('',#5898,#5902,#4598,.T.);
#7663=EDGE_CURVE('',#5903,#5902,#4599,.T.);
#7664=EDGE_CURVE('',#5904,#5903,#801,.T.);
#7665=EDGE_CURVE('',#5904,#5905,#4600,.T.);
#7666=EDGE_CURVE('',#5906,#5905,#802,.T.);
#7667=EDGE_CURVE('',#5902,#5906,#4601,.T.);
#7668=EDGE_CURVE('',#5907,#5907,#4602,.T.);
#7669=EDGE_CURVE('',#5908,#5908,#4603,.T.);
#7670=EDGE_CURVE('',#5909,#5909,#4604,.T.);
#7671=EDGE_CURVE('',#5909,#5910,#4605,.T.);
#7672=EDGE_CURVE('',#5910,#5910,#4606,.T.);
#7673=EDGE_CURVE('',#5911,#5912,#803,.T.);
#7674=EDGE_CURVE('',#5913,#5912,#804,.T.);
#7675=EDGE_CURVE('',#5914,#5913,#805,.T.);
#7676=EDGE_CURVE('',#5911,#5914,#806,.T.);
#7677=EDGE_CURVE('',#5915,#5916,#807,.T.);
#7678=EDGE_CURVE('',#5917,#5916,#808,.T.);
#7679=EDGE_CURVE('',#5918,#5917,#809,.T.);
#7680=EDGE_CURVE('',#5915,#5918,#810,.T.);
#7681=EDGE_CURVE('',#5919,#5920,#4607,.T.);
#7682=EDGE_CURVE('',#5921,#5919,#811,.T.);
#7683=EDGE_CURVE('',#5921,#5922,#4608,.T.);
#7684=EDGE_CURVE('',#5923,#5922,#812,.T.);
#7685=EDGE_CURVE('',#5920,#5923,#4609,.T.);
#7686=EDGE_CURVE('',#5920,#5924,#4610,.T.);
#7687=EDGE_CURVE('',#5925,#5924,#4611,.T.);
#7688=EDGE_CURVE('',#5926,#5925,#813,.T.);
#7689=EDGE_CURVE('',#5926,#5927,#4612,.T.);
#7690=EDGE_CURVE('',#5928,#5927,#814,.T.);
#7691=EDGE_CURVE('',#5924,#5928,#4613,.T.);
#7692=EDGE_CURVE('',#5929,#5929,#4614,.T.);
#7693=EDGE_CURVE('',#5930,#5930,#4615,.T.);
#7694=EDGE_CURVE('',#5931,#5931,#4616,.T.);
#7695=EDGE_CURVE('',#5931,#5932,#4617,.T.);
#7696=EDGE_CURVE('',#5932,#5932,#4618,.T.);
#7697=EDGE_CURVE('',#5933,#5934,#815,.T.);
#7698=EDGE_CURVE('',#5935,#5934,#816,.T.);
#7699=EDGE_CURVE('',#5936,#5935,#817,.T.);
#7700=EDGE_CURVE('',#5933,#5936,#818,.T.);
#7701=EDGE_CURVE('',#5937,#5938,#819,.T.);
#7702=EDGE_CURVE('',#5939,#5938,#820,.T.);
#7703=EDGE_CURVE('',#5940,#5939,#821,.T.);
#7704=EDGE_CURVE('',#5937,#5940,#822,.T.);
#7705=EDGE_CURVE('',#5941,#5942,#4619,.T.);
#7706=EDGE_CURVE('',#5943,#5941,#823,.T.);
#7707=EDGE_CURVE('',#5943,#5944,#4620,.T.);
#7708=EDGE_CURVE('',#5945,#5944,#824,.T.);
#7709=EDGE_CURVE('',#5942,#5945,#4621,.T.);
#7710=EDGE_CURVE('',#5942,#5946,#4622,.T.);
#7711=EDGE_CURVE('',#5947,#5946,#4623,.T.);
#7712=EDGE_CURVE('',#5948,#5947,#825,.T.);
#7713=EDGE_CURVE('',#5948,#5949,#4624,.T.);
#7714=EDGE_CURVE('',#5950,#5949,#826,.T.);
#7715=EDGE_CURVE('',#5946,#5950,#4625,.T.);
#7716=EDGE_CURVE('',#5951,#5951,#4626,.T.);
#7717=EDGE_CURVE('',#5952,#5952,#4627,.T.);
#7718=EDGE_CURVE('',#5953,#5953,#4628,.T.);
#7719=EDGE_CURVE('',#5953,#5954,#4629,.T.);
#7720=EDGE_CURVE('',#5954,#5954,#4630,.T.);
#7721=EDGE_CURVE('',#5955,#5956,#827,.T.);
#7722=EDGE_CURVE('',#5957,#5956,#828,.T.);
#7723=EDGE_CURVE('',#5958,#5957,#829,.T.);
#7724=EDGE_CURVE('',#5955,#5958,#830,.T.);
#7725=EDGE_CURVE('',#5959,#5960,#831,.T.);
#7726=EDGE_CURVE('',#5961,#5960,#832,.T.);
#7727=EDGE_CURVE('',#5962,#5961,#833,.T.);
#7728=EDGE_CURVE('',#5959,#5962,#834,.T.);
#7729=EDGE_CURVE('',#5963,#5964,#4631,.T.);
#7730=EDGE_CURVE('',#5965,#5963,#835,.T.);
#7731=EDGE_CURVE('',#5965,#5966,#4632,.T.);
#7732=EDGE_CURVE('',#5967,#5966,#836,.T.);
#7733=EDGE_CURVE('',#5964,#5967,#4633,.T.);
#7734=EDGE_CURVE('',#5964,#5968,#4634,.T.);
#7735=EDGE_CURVE('',#5969,#5968,#4635,.T.);
#7736=EDGE_CURVE('',#5970,#5969,#837,.T.);
#7737=EDGE_CURVE('',#5970,#5971,#4636,.T.);
#7738=EDGE_CURVE('',#5972,#5971,#838,.T.);
#7739=EDGE_CURVE('',#5968,#5972,#4637,.T.);
#7740=EDGE_CURVE('',#5973,#5973,#4638,.T.);
#7741=EDGE_CURVE('',#5974,#5974,#4639,.T.);
#7742=EDGE_CURVE('',#5975,#5975,#4640,.T.);
#7743=EDGE_CURVE('',#5975,#5976,#4641,.T.);
#7744=EDGE_CURVE('',#5976,#5976,#4642,.T.);
#7745=EDGE_CURVE('',#5977,#5978,#839,.T.);
#7746=EDGE_CURVE('',#5978,#5979,#840,.T.);
#7747=EDGE_CURVE('',#5979,#5980,#841,.T.);
#7748=EDGE_CURVE('',#5977,#5980,#842,.T.);
#7749=EDGE_CURVE('',#5981,#5982,#843,.T.);
#7750=EDGE_CURVE('',#5983,#5982,#844,.T.);
#7751=EDGE_CURVE('',#5984,#5983,#845,.T.);
#7752=EDGE_CURVE('',#5981,#5984,#846,.T.);
#7753=EDGE_CURVE('',#5985,#5986,#4643,.T.);
#7754=EDGE_CURVE('',#5986,#5987,#4644,.T.);
#7755=EDGE_CURVE('',#5988,#5987,#4645,.T.);
#7756=EDGE_CURVE('',#5989,#5988,#847,.T.);
#7757=EDGE_CURVE('',#5989,#5990,#4646,.T.);
#7758=EDGE_CURVE('',#5991,#5990,#848,.T.);
#7759=EDGE_CURVE('',#5987,#5991,#4647,.T.);
#7760=EDGE_CURVE('',#5986,#5992,#4648,.T.);
#7761=EDGE_CURVE('',#5992,#5993,#849,.T.);
#7762=EDGE_CURVE('',#5994,#5993,#4649,.T.);
#7763=EDGE_CURVE('',#5994,#5985,#850,.T.);
#7764=EDGE_CURVE('',#5995,#5995,#4650,.T.);
#7765=EDGE_CURVE('',#5996,#5996,#4651,.T.);
#7766=EDGE_CURVE('',#5997,#5998,#4652,.T.);
#7767=EDGE_CURVE('',#5999,#5997,#851,.T.);
#7768=EDGE_CURVE('',#5999,#6000,#4653,.T.);
#7769=EDGE_CURVE('',#6001,#6000,#852,.T.);
#7770=EDGE_CURVE('',#5998,#6001,#4654,.T.);
#7771=EDGE_CURVE('',#5998,#6002,#4655,.T.);
#7772=EDGE_CURVE('',#6003,#6002,#4656,.T.);
#7773=EDGE_CURVE('',#6004,#6003,#853,.T.);
#7774=EDGE_CURVE('',#6004,#6005,#4657,.T.);
#7775=EDGE_CURVE('',#6006,#6005,#854,.T.);
#7776=EDGE_CURVE('',#6002,#6006,#4658,.T.);
#7777=EDGE_CURVE('',#6007,#6007,#4659,.T.);
#7778=EDGE_CURVE('',#6008,#6008,#4660,.T.);
#7779=EDGE_CURVE('',#6009,#6009,#4661,.T.);
#7780=EDGE_CURVE('',#6009,#6010,#4662,.T.);
#7781=EDGE_CURVE('',#6010,#6010,#4663,.T.);
#7782=EDGE_CURVE('',#6011,#6012,#855,.T.);
#7783=EDGE_CURVE('',#6013,#6012,#856,.T.);
#7784=EDGE_CURVE('',#6014,#6013,#857,.T.);
#7785=EDGE_CURVE('',#6011,#6014,#858,.T.);
#7786=EDGE_CURVE('',#6015,#6016,#859,.T.);
#7787=EDGE_CURVE('',#6017,#6016,#860,.T.);
#7788=EDGE_CURVE('',#6018,#6017,#861,.T.);
#7789=EDGE_CURVE('',#6015,#6018,#862,.T.);
#7790=EDGE_CURVE('',#6017,#5979,#4664,.T.);
#7791=EDGE_CURVE('',#6016,#5980,#4665,.T.);
#7792=EDGE_CURVE('',#5977,#6015,#4666,.T.);
#7793=EDGE_CURVE('',#5978,#6018,#4667,.T.);
#7794=EDGE_CURVE('',#6000,#6004,#4668,.T.);
#7795=EDGE_CURVE('',#6005,#5999,#4669,.T.);
#7796=EDGE_CURVE('',#6006,#5997,#4670,.T.);
#7797=EDGE_CURVE('',#6001,#6003,#4671,.T.);
#7798=EDGE_CURVE('',#5957,#5984,#4672,.T.);
#7799=EDGE_CURVE('',#5983,#5958,#4673,.T.);
#7800=EDGE_CURVE('',#5982,#5955,#4674,.T.);
#7801=EDGE_CURVE('',#5956,#5981,#4675,.T.);
#7802=EDGE_CURVE('',#5967,#5969,#4676,.T.);
#7803=EDGE_CURVE('',#5966,#5970,#4677,.T.);
#7804=EDGE_CURVE('',#5971,#5965,#4678,.T.);
#7805=EDGE_CURVE('',#5972,#5963,#4679,.T.);
#7806=EDGE_CURVE('',#5935,#5962,#4680,.T.);
#7807=EDGE_CURVE('',#5961,#5936,#4681,.T.);
#7808=EDGE_CURVE('',#5960,#5933,#4682,.T.);
#7809=EDGE_CURVE('',#5934,#5959,#4683,.T.);
#7810=EDGE_CURVE('',#5945,#5947,#4684,.T.);
#7811=EDGE_CURVE('',#5944,#5948,#4685,.T.);
#7812=EDGE_CURVE('',#5949,#5943,#4686,.T.);
#7813=EDGE_CURVE('',#5950,#5941,#4687,.T.);
#7814=EDGE_CURVE('',#5913,#5940,#4688,.T.);
#7815=EDGE_CURVE('',#5939,#5914,#4689,.T.);
#7816=EDGE_CURVE('',#5938,#5911,#4690,.T.);
#7817=EDGE_CURVE('',#5912,#5937,#4691,.T.);
#7818=EDGE_CURVE('',#5923,#5925,#4692,.T.);
#7819=EDGE_CURVE('',#5922,#5926,#4693,.T.);
#7820=EDGE_CURVE('',#5927,#5921,#4694,.T.);
#7821=EDGE_CURVE('',#5928,#5919,#4695,.T.);
#7822=EDGE_CURVE('',#5891,#5918,#4696,.T.);
#7823=EDGE_CURVE('',#5917,#5892,#4697,.T.);
#7824=EDGE_CURVE('',#5916,#5889,#4698,.T.);
#7825=EDGE_CURVE('',#5890,#5915,#4699,.T.);
#7826=EDGE_CURVE('',#5901,#5903,#4700,.T.);
#7827=EDGE_CURVE('',#5900,#5904,#4701,.T.);
#7828=EDGE_CURVE('',#5905,#5899,#4702,.T.);
#7829=EDGE_CURVE('',#5906,#5897,#4703,.T.);
#7830=EDGE_CURVE('',#5869,#5896,#4704,.T.);
#7831=EDGE_CURVE('',#5895,#5870,#4705,.T.);
#7832=EDGE_CURVE('',#5894,#5867,#4706,.T.);
#7833=EDGE_CURVE('',#5868,#5893,#4707,.T.);
#7834=EDGE_CURVE('',#5879,#5881,#4708,.T.);
#7835=EDGE_CURVE('',#5878,#5882,#4709,.T.);
#7836=EDGE_CURVE('',#5883,#5877,#4710,.T.);
#7837=EDGE_CURVE('',#5884,#5875,#4711,.T.);
#7838=EDGE_CURVE('',#6013,#5874,#4712,.T.);
#7839=EDGE_CURVE('',#5873,#6014,#4713,.T.);
#7840=EDGE_CURVE('',#5872,#6011,#4714,.T.);
#7841=EDGE_CURVE('',#6012,#5871,#4715,.T.);
#7842=EDGE_CURVE('',#5990,#5993,#4716,.T.);
#7843=EDGE_CURVE('',#5994,#5989,#4717,.T.);
#7844=EDGE_CURVE('',#5985,#5988,#4718,.T.);
#7845=EDGE_CURVE('',#5991,#5992,#4719,.T.);
#10791=ORIENTED_EDGE('',*,*,#7557,.T.);
#10792=ORIENTED_EDGE('',*,*,#7558,.T.);
#10793=ORIENTED_EDGE('',*,*,#7559,.F.);
#10794=ORIENTED_EDGE('',*,*,#7558,.F.);
#10795=ORIENTED_EDGE('',*,*,#7560,.T.);
#10796=ORIENTED_EDGE('',*,*,#7561,.T.);
#10797=ORIENTED_EDGE('',*,*,#7562,.T.);
#10798=ORIENTED_EDGE('',*,*,#7563,.T.);
#10799=ORIENTED_EDGE('',*,*,#7561,.F.);
#10800=ORIENTED_EDGE('',*,*,#7564,.T.);
#10801=ORIENTED_EDGE('',*,*,#7565,.T.);
#10802=ORIENTED_EDGE('',*,*,#7566,.T.);
#10803=ORIENTED_EDGE('',*,*,#7567,.T.);
#10804=ORIENTED_EDGE('',*,*,#7566,.F.);
#10805=ORIENTED_EDGE('',*,*,#7568,.T.);
#10806=ORIENTED_EDGE('',*,*,#7560,.F.);
#10807=ORIENTED_EDGE('',*,*,#7569,.T.);
#10808=ORIENTED_EDGE('',*,*,#7570,.F.);
#10809=ORIENTED_EDGE('',*,*,#7569,.F.);
#10810=ORIENTED_EDGE('',*,*,#7564,.F.);
#10811=ORIENTED_EDGE('',*,*,#7563,.F.);
#10812=ORIENTED_EDGE('',*,*,#7571,.T.);
#10813=ORIENTED_EDGE('',*,*,#7568,.F.);
#10814=ORIENTED_EDGE('',*,*,#7565,.F.);
#10815=ORIENTED_EDGE('',*,*,#7571,.F.);
#10816=ORIENTED_EDGE('',*,*,#7562,.F.);
#10817=ORIENTED_EDGE('',*,*,#7567,.F.);
#10818=ORIENTED_EDGE('',*,*,#7572,.T.);
#10819=ORIENTED_EDGE('',*,*,#7573,.T.);
#10820=ORIENTED_EDGE('',*,*,#7572,.F.);
#10821=ORIENTED_EDGE('',*,*,#7574,.F.);
#10822=ORIENTED_EDGE('',*,*,#7575,.T.);
#10823=ORIENTED_EDGE('',*,*,#7559,.T.);
#10824=ORIENTED_EDGE('',*,*,#7575,.F.);
#10825=ORIENTED_EDGE('',*,*,#7557,.F.);
#10826=ORIENTED_EDGE('',*,*,#7576,.T.);
#10827=ORIENTED_EDGE('',*,*,#7577,.T.);
#10828=ORIENTED_EDGE('',*,*,#7576,.F.);
#10829=ORIENTED_EDGE('',*,*,#7577,.F.);
#10830=ORIENTED_EDGE('',*,*,#7570,.T.);
#10831=ORIENTED_EDGE('',*,*,#7574,.T.);
#10832=ORIENTED_EDGE('',*,*,#7573,.F.);
#10833=ORIENTED_EDGE('',*,*,#7578,.T.);
#10834=ORIENTED_EDGE('',*,*,#7578,.F.);
#10835=ORIENTED_EDGE('',*,*,#7579,.T.);
#10836=ORIENTED_EDGE('',*,*,#7579,.F.);
#10837=ORIENTED_EDGE('',*,*,#7580,.T.);
#10838=ORIENTED_EDGE('',*,*,#7580,.F.);
#10839=ORIENTED_EDGE('',*,*,#7581,.T.);
#10840=ORIENTED_EDGE('',*,*,#7581,.F.);
#10841=ORIENTED_EDGE('',*,*,#7582,.T.);
#10842=ORIENTED_EDGE('',*,*,#7582,.F.);
#10843=ORIENTED_EDGE('',*,*,#7583,.T.);
#10844=ORIENTED_EDGE('',*,*,#7583,.F.);
#10845=ORIENTED_EDGE('',*,*,#7584,.T.);
#10846=ORIENTED_EDGE('',*,*,#7584,.F.);
#10847=ORIENTED_EDGE('',*,*,#7585,.T.);
#10848=ORIENTED_EDGE('',*,*,#7586,.T.);
#10849=ORIENTED_EDGE('',*,*,#7587,.T.);
#10850=ORIENTED_EDGE('',*,*,#7588,.T.);
#10851=ORIENTED_EDGE('',*,*,#7586,.F.);
#10852=ORIENTED_EDGE('',*,*,#7589,.T.);
#10853=ORIENTED_EDGE('',*,*,#7590,.T.);
#10854=ORIENTED_EDGE('',*,*,#7591,.T.);
#10855=ORIENTED_EDGE('',*,*,#7590,.F.);
#10856=ORIENTED_EDGE('',*,*,#7592,.T.);
#10857=ORIENTED_EDGE('',*,*,#7593,.T.);
#10858=ORIENTED_EDGE('',*,*,#7594,.T.);
#10859=ORIENTED_EDGE('',*,*,#7593,.F.);
#10860=ORIENTED_EDGE('',*,*,#7595,.T.);
#10861=ORIENTED_EDGE('',*,*,#7596,.T.);
#10862=ORIENTED_EDGE('',*,*,#7597,.T.);
#10863=ORIENTED_EDGE('',*,*,#7596,.F.);
#10864=ORIENTED_EDGE('',*,*,#7598,.T.);
#10865=ORIENTED_EDGE('',*,*,#7599,.F.);
#10866=ORIENTED_EDGE('',*,*,#7600,.T.);
#10867=ORIENTED_EDGE('',*,*,#7601,.T.);
#10868=ORIENTED_EDGE('',*,*,#7600,.F.);
#10869=ORIENTED_EDGE('',*,*,#7588,.F.);
#10870=ORIENTED_EDGE('',*,*,#7602,.T.);
#10871=ORIENTED_EDGE('',*,*,#7603,.T.);
#10872=ORIENTED_EDGE('',*,*,#7602,.F.);
#10873=ORIENTED_EDGE('',*,*,#7587,.F.);
#10874=ORIENTED_EDGE('',*,*,#7604,.F.);
#10875=ORIENTED_EDGE('',*,*,#7605,.T.);
#10876=ORIENTED_EDGE('',*,*,#7598,.F.);
#10877=ORIENTED_EDGE('',*,*,#7595,.F.);
#10878=ORIENTED_EDGE('',*,*,#7605,.F.);
#10879=ORIENTED_EDGE('',*,*,#7604,.T.);
#10880=ORIENTED_EDGE('',*,*,#7606,.T.);
#10881=ORIENTED_EDGE('',*,*,#7607,.F.);
#10882=ORIENTED_EDGE('',*,*,#7606,.F.);
#10883=ORIENTED_EDGE('',*,*,#7589,.F.);
#10884=ORIENTED_EDGE('',*,*,#7608,.T.);
#10885=ORIENTED_EDGE('',*,*,#7607,.T.);
#10886=ORIENTED_EDGE('',*,*,#7608,.F.);
#10887=ORIENTED_EDGE('',*,*,#7609,.F.);
#10888=ORIENTED_EDGE('',*,*,#7610,.T.);
#10889=ORIENTED_EDGE('',*,*,#7594,.F.);
#10890=ORIENTED_EDGE('',*,*,#7610,.F.);
#10891=ORIENTED_EDGE('',*,*,#7611,.F.);
#10892=ORIENTED_EDGE('',*,*,#7612,.T.);
#10893=ORIENTED_EDGE('',*,*,#7613,.T.);
#10894=ORIENTED_EDGE('',*,*,#7612,.F.);
#10895=ORIENTED_EDGE('',*,*,#7614,.T.);
#10896=ORIENTED_EDGE('',*,*,#7615,.T.);
#10897=ORIENTED_EDGE('',*,*,#7616,.F.);
#10898=ORIENTED_EDGE('',*,*,#7615,.F.);
#10899=ORIENTED_EDGE('',*,*,#7617,.F.);
#10900=ORIENTED_EDGE('',*,*,#7618,.F.);
#10901=ORIENTED_EDGE('',*,*,#7619,.T.);
#10902=ORIENTED_EDGE('',*,*,#7620,.T.);
#10903=ORIENTED_EDGE('',*,*,#7619,.F.);
#10904=ORIENTED_EDGE('',*,*,#7614,.F.);
#10905=ORIENTED_EDGE('',*,*,#7621,.T.);
#10906=ORIENTED_EDGE('',*,*,#7617,.T.);
#10907=ORIENTED_EDGE('',*,*,#7618,.T.);
#10908=ORIENTED_EDGE('',*,*,#7621,.F.);
#10909=ORIENTED_EDGE('',*,*,#7620,.F.);
#10910=ORIENTED_EDGE('',*,*,#7585,.F.);
#10911=ORIENTED_EDGE('',*,*,#7616,.T.);
#10912=ORIENTED_EDGE('',*,*,#7592,.F.);
#10913=ORIENTED_EDGE('',*,*,#7611,.T.);
#10914=ORIENTED_EDGE('',*,*,#7597,.F.);
#10915=ORIENTED_EDGE('',*,*,#7613,.F.);
#10916=ORIENTED_EDGE('',*,*,#7609,.T.);
#10917=ORIENTED_EDGE('',*,*,#7599,.T.);
#10918=ORIENTED_EDGE('',*,*,#7603,.F.);
#10919=ORIENTED_EDGE('',*,*,#7601,.F.);
#10920=ORIENTED_EDGE('',*,*,#7591,.F.);
#10921=ORIENTED_EDGE('',*,*,#7622,.T.);
#10922=ORIENTED_EDGE('',*,*,#7623,.T.);
#10923=ORIENTED_EDGE('',*,*,#7624,.F.);
#10924=ORIENTED_EDGE('',*,*,#7623,.F.);
#10925=ORIENTED_EDGE('',*,*,#7625,.T.);
#10926=ORIENTED_EDGE('',*,*,#7626,.F.);
#10927=ORIENTED_EDGE('',*,*,#7627,.F.);
#10928=ORIENTED_EDGE('',*,*,#7628,.F.);
#10929=ORIENTED_EDGE('',*,*,#7629,.T.);
#10930=ORIENTED_EDGE('',*,*,#7630,.F.);
#10931=ORIENTED_EDGE('',*,*,#7631,.F.);
#10932=ORIENTED_EDGE('',*,*,#7632,.F.);
#10933=ORIENTED_EDGE('',*,*,#7633,.F.);
#10934=ORIENTED_EDGE('',*,*,#7634,.F.);
#10935=ORIENTED_EDGE('',*,*,#7635,.T.);
#10936=ORIENTED_EDGE('',*,*,#7636,.F.);
#10937=ORIENTED_EDGE('',*,*,#7637,.F.);
#10938=ORIENTED_EDGE('',*,*,#7638,.T.);
#10939=ORIENTED_EDGE('',*,*,#7639,.F.);
#10940=ORIENTED_EDGE('',*,*,#7640,.F.);
#10941=ORIENTED_EDGE('',*,*,#7641,.T.);
#10942=ORIENTED_EDGE('',*,*,#7642,.F.);
#10943=ORIENTED_EDGE('',*,*,#7643,.F.);
#10944=ORIENTED_EDGE('',*,*,#7638,.F.);
#10945=ORIENTED_EDGE('',*,*,#7644,.T.);
#10946=ORIENTED_EDGE('',*,*,#7645,.F.);
#10947=ORIENTED_EDGE('',*,*,#7646,.T.);
#10948=ORIENTED_EDGE('',*,*,#7647,.T.);
#10949=ORIENTED_EDGE('',*,*,#7648,.F.);
#10950=ORIENTED_EDGE('',*,*,#7647,.F.);
#10951=ORIENTED_EDGE('',*,*,#7649,.T.);
#10952=ORIENTED_EDGE('',*,*,#7650,.F.);
#10953=ORIENTED_EDGE('',*,*,#7651,.F.);
#10954=ORIENTED_EDGE('',*,*,#7652,.F.);
#10955=ORIENTED_EDGE('',*,*,#7653,.T.);
#10956=ORIENTED_EDGE('',*,*,#7654,.F.);
#10957=ORIENTED_EDGE('',*,*,#7655,.F.);
#10958=ORIENTED_EDGE('',*,*,#7656,.F.);
#10959=ORIENTED_EDGE('',*,*,#7657,.F.);
#10960=ORIENTED_EDGE('',*,*,#7658,.F.);
#10961=ORIENTED_EDGE('',*,*,#7659,.T.);
#10962=ORIENTED_EDGE('',*,*,#7660,.F.);
#10963=ORIENTED_EDGE('',*,*,#7661,.F.);
#10964=ORIENTED_EDGE('',*,*,#7662,.T.);
#10965=ORIENTED_EDGE('',*,*,#7663,.F.);
#10966=ORIENTED_EDGE('',*,*,#7664,.F.);
#10967=ORIENTED_EDGE('',*,*,#7665,.T.);
#10968=ORIENTED_EDGE('',*,*,#7666,.F.);
#10969=ORIENTED_EDGE('',*,*,#7667,.F.);
#10970=ORIENTED_EDGE('',*,*,#7662,.F.);
#10971=ORIENTED_EDGE('',*,*,#7668,.T.);
#10972=ORIENTED_EDGE('',*,*,#7669,.F.);
#10973=ORIENTED_EDGE('',*,*,#7670,.T.);
#10974=ORIENTED_EDGE('',*,*,#7671,.T.);
#10975=ORIENTED_EDGE('',*,*,#7672,.F.);
#10976=ORIENTED_EDGE('',*,*,#7671,.F.);
#10977=ORIENTED_EDGE('',*,*,#7673,.T.);
#10978=ORIENTED_EDGE('',*,*,#7674,.F.);
#10979=ORIENTED_EDGE('',*,*,#7675,.F.);
#10980=ORIENTED_EDGE('',*,*,#7676,.F.);
#10981=ORIENTED_EDGE('',*,*,#7677,.T.);
#10982=ORIENTED_EDGE('',*,*,#7678,.F.);
#10983=ORIENTED_EDGE('',*,*,#7679,.F.);
#10984=ORIENTED_EDGE('',*,*,#7680,.F.);
#10985=ORIENTED_EDGE('',*,*,#7681,.F.);
#10986=ORIENTED_EDGE('',*,*,#7682,.F.);
#10987=ORIENTED_EDGE('',*,*,#7683,.T.);
#10988=ORIENTED_EDGE('',*,*,#7684,.F.);
#10989=ORIENTED_EDGE('',*,*,#7685,.F.);
#10990=ORIENTED_EDGE('',*,*,#7686,.T.);
#10991=ORIENTED_EDGE('',*,*,#7687,.F.);
#10992=ORIENTED_EDGE('',*,*,#7688,.F.);
#10993=ORIENTED_EDGE('',*,*,#7689,.T.);
#10994=ORIENTED_EDGE('',*,*,#7690,.F.);
#10995=ORIENTED_EDGE('',*,*,#7691,.F.);
#10996=ORIENTED_EDGE('',*,*,#7686,.F.);
#10997=ORIENTED_EDGE('',*,*,#7692,.T.);
#10998=ORIENTED_EDGE('',*,*,#7693,.F.);
#10999=ORIENTED_EDGE('',*,*,#7694,.T.);
#11000=ORIENTED_EDGE('',*,*,#7695,.T.);
#11001=ORIENTED_EDGE('',*,*,#7696,.F.);
#11002=ORIENTED_EDGE('',*,*,#7695,.F.);
#11003=ORIENTED_EDGE('',*,*,#7697,.T.);
#11004=ORIENTED_EDGE('',*,*,#7698,.F.);
#11005=ORIENTED_EDGE('',*,*,#7699,.F.);
#11006=ORIENTED_EDGE('',*,*,#7700,.F.);
#11007=ORIENTED_EDGE('',*,*,#7701,.T.);
#11008=ORIENTED_EDGE('',*,*,#7702,.F.);
#11009=ORIENTED_EDGE('',*,*,#7703,.F.);
#11010=ORIENTED_EDGE('',*,*,#7704,.F.);
#11011=ORIENTED_EDGE('',*,*,#7705,.F.);
#11012=ORIENTED_EDGE('',*,*,#7706,.F.);
#11013=ORIENTED_EDGE('',*,*,#7707,.T.);
#11014=ORIENTED_EDGE('',*,*,#7708,.F.);
#11015=ORIENTED_EDGE('',*,*,#7709,.F.);
#11016=ORIENTED_EDGE('',*,*,#7710,.T.);
#11017=ORIENTED_EDGE('',*,*,#7711,.F.);
#11018=ORIENTED_EDGE('',*,*,#7712,.F.);
#11019=ORIENTED_EDGE('',*,*,#7713,.T.);
#11020=ORIENTED_EDGE('',*,*,#7714,.F.);
#11021=ORIENTED_EDGE('',*,*,#7715,.F.);
#11022=ORIENTED_EDGE('',*,*,#7710,.F.);
#11023=ORIENTED_EDGE('',*,*,#7716,.T.);
#11024=ORIENTED_EDGE('',*,*,#7717,.F.);
#11025=ORIENTED_EDGE('',*,*,#7718,.T.);
#11026=ORIENTED_EDGE('',*,*,#7719,.T.);
#11027=ORIENTED_EDGE('',*,*,#7720,.F.);
#11028=ORIENTED_EDGE('',*,*,#7719,.F.);
#11029=ORIENTED_EDGE('',*,*,#7721,.T.);
#11030=ORIENTED_EDGE('',*,*,#7722,.F.);
#11031=ORIENTED_EDGE('',*,*,#7723,.F.);
#11032=ORIENTED_EDGE('',*,*,#7724,.F.);
#11033=ORIENTED_EDGE('',*,*,#7725,.T.);
#11034=ORIENTED_EDGE('',*,*,#7726,.F.);
#11035=ORIENTED_EDGE('',*,*,#7727,.F.);
#11036=ORIENTED_EDGE('',*,*,#7728,.F.);
#11037=ORIENTED_EDGE('',*,*,#7729,.F.);
#11038=ORIENTED_EDGE('',*,*,#7730,.F.);
#11039=ORIENTED_EDGE('',*,*,#7731,.T.);
#11040=ORIENTED_EDGE('',*,*,#7732,.F.);
#11041=ORIENTED_EDGE('',*,*,#7733,.F.);
#11042=ORIENTED_EDGE('',*,*,#7734,.T.);
#11043=ORIENTED_EDGE('',*,*,#7735,.F.);
#11044=ORIENTED_EDGE('',*,*,#7736,.F.);
#11045=ORIENTED_EDGE('',*,*,#7737,.T.);
#11046=ORIENTED_EDGE('',*,*,#7738,.F.);
#11047=ORIENTED_EDGE('',*,*,#7739,.F.);
#11048=ORIENTED_EDGE('',*,*,#7734,.F.);
#11049=ORIENTED_EDGE('',*,*,#7740,.T.);
#11050=ORIENTED_EDGE('',*,*,#7741,.F.);
#11051=ORIENTED_EDGE('',*,*,#7742,.T.);
#11052=ORIENTED_EDGE('',*,*,#7743,.T.);
#11053=ORIENTED_EDGE('',*,*,#7744,.F.);
#11054=ORIENTED_EDGE('',*,*,#7743,.F.);
#11055=ORIENTED_EDGE('',*,*,#7745,.T.);
#11056=ORIENTED_EDGE('',*,*,#7746,.T.);
#11057=ORIENTED_EDGE('',*,*,#7747,.T.);
#11058=ORIENTED_EDGE('',*,*,#7748,.F.);
#11059=ORIENTED_EDGE('',*,*,#7749,.T.);
#11060=ORIENTED_EDGE('',*,*,#7750,.F.);
#11061=ORIENTED_EDGE('',*,*,#7751,.F.);
#11062=ORIENTED_EDGE('',*,*,#7752,.F.);
#11063=ORIENTED_EDGE('',*,*,#7753,.T.);
#11064=ORIENTED_EDGE('',*,*,#7754,.T.);
#11065=ORIENTED_EDGE('',*,*,#7755,.F.);
#11066=ORIENTED_EDGE('',*,*,#7756,.F.);
#11067=ORIENTED_EDGE('',*,*,#7757,.T.);
#11068=ORIENTED_EDGE('',*,*,#7758,.F.);
#11069=ORIENTED_EDGE('',*,*,#7759,.F.);
#11070=ORIENTED_EDGE('',*,*,#7754,.F.);
#11071=ORIENTED_EDGE('',*,*,#7760,.T.);
#11072=ORIENTED_EDGE('',*,*,#7761,.T.);
#11073=ORIENTED_EDGE('',*,*,#7762,.F.);
#11074=ORIENTED_EDGE('',*,*,#7763,.T.);
#11075=ORIENTED_EDGE('',*,*,#7764,.T.);
#11076=ORIENTED_EDGE('',*,*,#7765,.F.);
#11077=ORIENTED_EDGE('',*,*,#7766,.F.);
#11078=ORIENTED_EDGE('',*,*,#7767,.F.);
#11079=ORIENTED_EDGE('',*,*,#7768,.T.);
#11080=ORIENTED_EDGE('',*,*,#7769,.F.);
#11081=ORIENTED_EDGE('',*,*,#7770,.F.);
#11082=ORIENTED_EDGE('',*,*,#7771,.T.);
#11083=ORIENTED_EDGE('',*,*,#7772,.F.);
#11084=ORIENTED_EDGE('',*,*,#7773,.F.);
#11085=ORIENTED_EDGE('',*,*,#7774,.T.);
#11086=ORIENTED_EDGE('',*,*,#7775,.F.);
#11087=ORIENTED_EDGE('',*,*,#7776,.F.);
#11088=ORIENTED_EDGE('',*,*,#7771,.F.);
#11089=ORIENTED_EDGE('',*,*,#7777,.T.);
#11090=ORIENTED_EDGE('',*,*,#7778,.F.);
#11091=ORIENTED_EDGE('',*,*,#7779,.T.);
#11092=ORIENTED_EDGE('',*,*,#7780,.T.);
#11093=ORIENTED_EDGE('',*,*,#7781,.F.);
#11094=ORIENTED_EDGE('',*,*,#7780,.F.);
#11095=ORIENTED_EDGE('',*,*,#7782,.T.);
#11096=ORIENTED_EDGE('',*,*,#7783,.F.);
#11097=ORIENTED_EDGE('',*,*,#7784,.F.);
#11098=ORIENTED_EDGE('',*,*,#7785,.F.);
#11099=ORIENTED_EDGE('',*,*,#7786,.T.);
#11100=ORIENTED_EDGE('',*,*,#7787,.F.);
#11101=ORIENTED_EDGE('',*,*,#7788,.F.);
#11102=ORIENTED_EDGE('',*,*,#7789,.F.);
#11103=ORIENTED_EDGE('',*,*,#7790,.F.);
#11104=ORIENTED_EDGE('',*,*,#7787,.T.);
#11105=ORIENTED_EDGE('',*,*,#7791,.T.);
#11106=ORIENTED_EDGE('',*,*,#7747,.F.);
#11107=ORIENTED_EDGE('',*,*,#7792,.T.);
#11108=ORIENTED_EDGE('',*,*,#7789,.T.);
#11109=ORIENTED_EDGE('',*,*,#7793,.F.);
#11110=ORIENTED_EDGE('',*,*,#7745,.F.);
#11111=ORIENTED_EDGE('',*,*,#7748,.T.);
#11112=ORIENTED_EDGE('',*,*,#7791,.F.);
#11113=ORIENTED_EDGE('',*,*,#7786,.F.);
#11114=ORIENTED_EDGE('',*,*,#7792,.F.);
#11115=ORIENTED_EDGE('',*,*,#7793,.T.);
#11116=ORIENTED_EDGE('',*,*,#7788,.T.);
#11117=ORIENTED_EDGE('',*,*,#7790,.T.);
#11118=ORIENTED_EDGE('',*,*,#7746,.F.);
#11119=ORIENTED_EDGE('',*,*,#7779,.F.);
#11120=ORIENTED_EDGE('',*,*,#7778,.T.);
#11121=ORIENTED_EDGE('',*,*,#7781,.T.);
#11122=ORIENTED_EDGE('',*,*,#7777,.F.);
#11123=ORIENTED_EDGE('',*,*,#7794,.F.);
#11124=ORIENTED_EDGE('',*,*,#7768,.F.);
#11125=ORIENTED_EDGE('',*,*,#7795,.F.);
#11126=ORIENTED_EDGE('',*,*,#7774,.F.);
#11127=ORIENTED_EDGE('',*,*,#7772,.T.);
#11128=ORIENTED_EDGE('',*,*,#7776,.T.);
#11129=ORIENTED_EDGE('',*,*,#7796,.T.);
#11130=ORIENTED_EDGE('',*,*,#7766,.T.);
#11131=ORIENTED_EDGE('',*,*,#7770,.T.);
#11132=ORIENTED_EDGE('',*,*,#7797,.T.);
#11133=ORIENTED_EDGE('',*,*,#7775,.T.);
#11134=ORIENTED_EDGE('',*,*,#7795,.T.);
#11135=ORIENTED_EDGE('',*,*,#7767,.T.);
#11136=ORIENTED_EDGE('',*,*,#7796,.F.);
#11137=ORIENTED_EDGE('',*,*,#7773,.T.);
#11138=ORIENTED_EDGE('',*,*,#7797,.F.);
#11139=ORIENTED_EDGE('',*,*,#7769,.T.);
#11140=ORIENTED_EDGE('',*,*,#7794,.T.);
#11141=ORIENTED_EDGE('',*,*,#7744,.T.);
#11142=ORIENTED_EDGE('',*,*,#7764,.F.);
#11143=ORIENTED_EDGE('',*,*,#7742,.F.);
#11144=ORIENTED_EDGE('',*,*,#7765,.T.);
#11145=ORIENTED_EDGE('',*,*,#7723,.T.);
#11146=ORIENTED_EDGE('',*,*,#7798,.T.);
#11147=ORIENTED_EDGE('',*,*,#7751,.T.);
#11148=ORIENTED_EDGE('',*,*,#7799,.T.);
#11149=ORIENTED_EDGE('',*,*,#7800,.F.);
#11150=ORIENTED_EDGE('',*,*,#7749,.F.);
#11151=ORIENTED_EDGE('',*,*,#7801,.F.);
#11152=ORIENTED_EDGE('',*,*,#7721,.F.);
#11153=ORIENTED_EDGE('',*,*,#7722,.T.);
#11154=ORIENTED_EDGE('',*,*,#7801,.T.);
#11155=ORIENTED_EDGE('',*,*,#7752,.T.);
#11156=ORIENTED_EDGE('',*,*,#7798,.F.);
#11157=ORIENTED_EDGE('',*,*,#7724,.T.);
#11158=ORIENTED_EDGE('',*,*,#7799,.F.);
#11159=ORIENTED_EDGE('',*,*,#7750,.T.);
#11160=ORIENTED_EDGE('',*,*,#7800,.T.);
#11161=ORIENTED_EDGE('',*,*,#7736,.T.);
#11162=ORIENTED_EDGE('',*,*,#7802,.F.);
#11163=ORIENTED_EDGE('',*,*,#7732,.T.);
#11164=ORIENTED_EDGE('',*,*,#7803,.T.);
#11165=ORIENTED_EDGE('',*,*,#7738,.T.);
#11166=ORIENTED_EDGE('',*,*,#7804,.T.);
#11167=ORIENTED_EDGE('',*,*,#7730,.T.);
#11168=ORIENTED_EDGE('',*,*,#7805,.F.);
#11169=ORIENTED_EDGE('',*,*,#7735,.T.);
#11170=ORIENTED_EDGE('',*,*,#7739,.T.);
#11171=ORIENTED_EDGE('',*,*,#7805,.T.);
#11172=ORIENTED_EDGE('',*,*,#7729,.T.);
#11173=ORIENTED_EDGE('',*,*,#7733,.T.);
#11174=ORIENTED_EDGE('',*,*,#7802,.T.);
#11175=ORIENTED_EDGE('',*,*,#7803,.F.);
#11176=ORIENTED_EDGE('',*,*,#7731,.F.);
#11177=ORIENTED_EDGE('',*,*,#7804,.F.);
#11178=ORIENTED_EDGE('',*,*,#7737,.F.);
#11179=ORIENTED_EDGE('',*,*,#7720,.T.);
#11180=ORIENTED_EDGE('',*,*,#7740,.F.);
#11181=ORIENTED_EDGE('',*,*,#7718,.F.);
#11182=ORIENTED_EDGE('',*,*,#7741,.T.);
#11183=ORIENTED_EDGE('',*,*,#7699,.T.);
#11184=ORIENTED_EDGE('',*,*,#7806,.T.);
#11185=ORIENTED_EDGE('',*,*,#7727,.T.);
#11186=ORIENTED_EDGE('',*,*,#7807,.T.);
#11187=ORIENTED_EDGE('',*,*,#7808,.F.);
#11188=ORIENTED_EDGE('',*,*,#7725,.F.);
#11189=ORIENTED_EDGE('',*,*,#7809,.F.);
#11190=ORIENTED_EDGE('',*,*,#7697,.F.);
#11191=ORIENTED_EDGE('',*,*,#7698,.T.);
#11192=ORIENTED_EDGE('',*,*,#7809,.T.);
#11193=ORIENTED_EDGE('',*,*,#7728,.T.);
#11194=ORIENTED_EDGE('',*,*,#7806,.F.);
#11195=ORIENTED_EDGE('',*,*,#7700,.T.);
#11196=ORIENTED_EDGE('',*,*,#7807,.F.);
#11197=ORIENTED_EDGE('',*,*,#7726,.T.);
#11198=ORIENTED_EDGE('',*,*,#7808,.T.);
#11199=ORIENTED_EDGE('',*,*,#7712,.T.);
#11200=ORIENTED_EDGE('',*,*,#7810,.F.);
#11201=ORIENTED_EDGE('',*,*,#7708,.T.);
#11202=ORIENTED_EDGE('',*,*,#7811,.T.);
#11203=ORIENTED_EDGE('',*,*,#7714,.T.);
#11204=ORIENTED_EDGE('',*,*,#7812,.T.);
#11205=ORIENTED_EDGE('',*,*,#7706,.T.);
#11206=ORIENTED_EDGE('',*,*,#7813,.F.);
#11207=ORIENTED_EDGE('',*,*,#7711,.T.);
#11208=ORIENTED_EDGE('',*,*,#7715,.T.);
#11209=ORIENTED_EDGE('',*,*,#7813,.T.);
#11210=ORIENTED_EDGE('',*,*,#7705,.T.);
#11211=ORIENTED_EDGE('',*,*,#7709,.T.);
#11212=ORIENTED_EDGE('',*,*,#7810,.T.);
#11213=ORIENTED_EDGE('',*,*,#7811,.F.);
#11214=ORIENTED_EDGE('',*,*,#7707,.F.);
#11215=ORIENTED_EDGE('',*,*,#7812,.F.);
#11216=ORIENTED_EDGE('',*,*,#7713,.F.);
#11217=ORIENTED_EDGE('',*,*,#7696,.T.);
#11218=ORIENTED_EDGE('',*,*,#7716,.F.);
#11219=ORIENTED_EDGE('',*,*,#7694,.F.);
#11220=ORIENTED_EDGE('',*,*,#7717,.T.);
#11221=ORIENTED_EDGE('',*,*,#7675,.T.);
#11222=ORIENTED_EDGE('',*,*,#7814,.T.);
#11223=ORIENTED_EDGE('',*,*,#7703,.T.);
#11224=ORIENTED_EDGE('',*,*,#7815,.T.);
#11225=ORIENTED_EDGE('',*,*,#7816,.F.);
#11226=ORIENTED_EDGE('',*,*,#7701,.F.);
#11227=ORIENTED_EDGE('',*,*,#7817,.F.);
#11228=ORIENTED_EDGE('',*,*,#7673,.F.);
#11229=ORIENTED_EDGE('',*,*,#7674,.T.);
#11230=ORIENTED_EDGE('',*,*,#7817,.T.);
#11231=ORIENTED_EDGE('',*,*,#7704,.T.);
#11232=ORIENTED_EDGE('',*,*,#7814,.F.);
#11233=ORIENTED_EDGE('',*,*,#7676,.T.);
#11234=ORIENTED_EDGE('',*,*,#7815,.F.);
#11235=ORIENTED_EDGE('',*,*,#7702,.T.);
#11236=ORIENTED_EDGE('',*,*,#7816,.T.);
#11237=ORIENTED_EDGE('',*,*,#7688,.T.);
#11238=ORIENTED_EDGE('',*,*,#7818,.F.);
#11239=ORIENTED_EDGE('',*,*,#7684,.T.);
#11240=ORIENTED_EDGE('',*,*,#7819,.T.);
#11241=ORIENTED_EDGE('',*,*,#7690,.T.);
#11242=ORIENTED_EDGE('',*,*,#7820,.T.);
#11243=ORIENTED_EDGE('',*,*,#7682,.T.);
#11244=ORIENTED_EDGE('',*,*,#7821,.F.);
#11245=ORIENTED_EDGE('',*,*,#7687,.T.);
#11246=ORIENTED_EDGE('',*,*,#7691,.T.);
#11247=ORIENTED_EDGE('',*,*,#7821,.T.);
#11248=ORIENTED_EDGE('',*,*,#7681,.T.);
#11249=ORIENTED_EDGE('',*,*,#7685,.T.);
#11250=ORIENTED_EDGE('',*,*,#7818,.T.);
#11251=ORIENTED_EDGE('',*,*,#7819,.F.);
#11252=ORIENTED_EDGE('',*,*,#7683,.F.);
#11253=ORIENTED_EDGE('',*,*,#7820,.F.);
#11254=ORIENTED_EDGE('',*,*,#7689,.F.);
#11255=ORIENTED_EDGE('',*,*,#7672,.T.);
#11256=ORIENTED_EDGE('',*,*,#7692,.F.);
#11257=ORIENTED_EDGE('',*,*,#7670,.F.);
#11258=ORIENTED_EDGE('',*,*,#7693,.T.);
#11259=ORIENTED_EDGE('',*,*,#7651,.T.);
#11260=ORIENTED_EDGE('',*,*,#7822,.T.);
#11261=ORIENTED_EDGE('',*,*,#7679,.T.);
#11262=ORIENTED_EDGE('',*,*,#7823,.T.);
#11263=ORIENTED_EDGE('',*,*,#7824,.F.);
#11264=ORIENTED_EDGE('',*,*,#7677,.F.);
#11265=ORIENTED_EDGE('',*,*,#7825,.F.);
#11266=ORIENTED_EDGE('',*,*,#7649,.F.);
#11267=ORIENTED_EDGE('',*,*,#7650,.T.);
#11268=ORIENTED_EDGE('',*,*,#7825,.T.);
#11269=ORIENTED_EDGE('',*,*,#7680,.T.);
#11270=ORIENTED_EDGE('',*,*,#7822,.F.);
#11271=ORIENTED_EDGE('',*,*,#7652,.T.);
#11272=ORIENTED_EDGE('',*,*,#7823,.F.);
#11273=ORIENTED_EDGE('',*,*,#7678,.T.);
#11274=ORIENTED_EDGE('',*,*,#7824,.T.);
#11275=ORIENTED_EDGE('',*,*,#7664,.T.);
#11276=ORIENTED_EDGE('',*,*,#7826,.F.);
#11277=ORIENTED_EDGE('',*,*,#7660,.T.);
#11278=ORIENTED_EDGE('',*,*,#7827,.T.);
#11279=ORIENTED_EDGE('',*,*,#7666,.T.);
#11280=ORIENTED_EDGE('',*,*,#7828,.T.);
#11281=ORIENTED_EDGE('',*,*,#7658,.T.);
#11282=ORIENTED_EDGE('',*,*,#7829,.F.);
#11283=ORIENTED_EDGE('',*,*,#7663,.T.);
#11284=ORIENTED_EDGE('',*,*,#7667,.T.);
#11285=ORIENTED_EDGE('',*,*,#7829,.T.);
#11286=ORIENTED_EDGE('',*,*,#7657,.T.);
#11287=ORIENTED_EDGE('',*,*,#7661,.T.);
#11288=ORIENTED_EDGE('',*,*,#7826,.T.);
#11289=ORIENTED_EDGE('',*,*,#7827,.F.);
#11290=ORIENTED_EDGE('',*,*,#7659,.F.);
#11291=ORIENTED_EDGE('',*,*,#7828,.F.);
#11292=ORIENTED_EDGE('',*,*,#7665,.F.);
#11293=ORIENTED_EDGE('',*,*,#7648,.T.);
#11294=ORIENTED_EDGE('',*,*,#7668,.F.);
#11295=ORIENTED_EDGE('',*,*,#7646,.F.);
#11296=ORIENTED_EDGE('',*,*,#7669,.T.);
#11297=ORIENTED_EDGE('',*,*,#7627,.T.);
#11298=ORIENTED_EDGE('',*,*,#7830,.T.);
#11299=ORIENTED_EDGE('',*,*,#7655,.T.);
#11300=ORIENTED_EDGE('',*,*,#7831,.T.);
#11301=ORIENTED_EDGE('',*,*,#7832,.F.);
#11302=ORIENTED_EDGE('',*,*,#7653,.F.);
#11303=ORIENTED_EDGE('',*,*,#7833,.F.);
#11304=ORIENTED_EDGE('',*,*,#7625,.F.);
#11305=ORIENTED_EDGE('',*,*,#7626,.T.);
#11306=ORIENTED_EDGE('',*,*,#7833,.T.);
#11307=ORIENTED_EDGE('',*,*,#7656,.T.);
#11308=ORIENTED_EDGE('',*,*,#7830,.F.);
#11309=ORIENTED_EDGE('',*,*,#7628,.T.);
#11310=ORIENTED_EDGE('',*,*,#7831,.F.);
#11311=ORIENTED_EDGE('',*,*,#7654,.T.);
#11312=ORIENTED_EDGE('',*,*,#7832,.T.);
#11313=ORIENTED_EDGE('',*,*,#7640,.T.);
#11314=ORIENTED_EDGE('',*,*,#7834,.F.);
#11315=ORIENTED_EDGE('',*,*,#7636,.T.);
#11316=ORIENTED_EDGE('',*,*,#7835,.T.);
#11317=ORIENTED_EDGE('',*,*,#7642,.T.);
#11318=ORIENTED_EDGE('',*,*,#7836,.T.);
#11319=ORIENTED_EDGE('',*,*,#7634,.T.);
#11320=ORIENTED_EDGE('',*,*,#7837,.F.);
#11321=ORIENTED_EDGE('',*,*,#7639,.T.);
#11322=ORIENTED_EDGE('',*,*,#7643,.T.);
#11323=ORIENTED_EDGE('',*,*,#7837,.T.);
#11324=ORIENTED_EDGE('',*,*,#7633,.T.);
#11325=ORIENTED_EDGE('',*,*,#7637,.T.);
#11326=ORIENTED_EDGE('',*,*,#7834,.T.);
#11327=ORIENTED_EDGE('',*,*,#7835,.F.);
#11328=ORIENTED_EDGE('',*,*,#7635,.F.);
#11329=ORIENTED_EDGE('',*,*,#7836,.F.);
#11330=ORIENTED_EDGE('',*,*,#7641,.F.);
#11331=ORIENTED_EDGE('',*,*,#7624,.T.);
#11332=ORIENTED_EDGE('',*,*,#7644,.F.);
#11333=ORIENTED_EDGE('',*,*,#7622,.F.);
#11334=ORIENTED_EDGE('',*,*,#7645,.T.);
#11335=ORIENTED_EDGE('',*,*,#7784,.T.);
#11336=ORIENTED_EDGE('',*,*,#7838,.T.);
#11337=ORIENTED_EDGE('',*,*,#7631,.T.);
#11338=ORIENTED_EDGE('',*,*,#7839,.T.);
#11339=ORIENTED_EDGE('',*,*,#7840,.F.);
#11340=ORIENTED_EDGE('',*,*,#7629,.F.);
#11341=ORIENTED_EDGE('',*,*,#7841,.F.);
#11342=ORIENTED_EDGE('',*,*,#7782,.F.);
#11343=ORIENTED_EDGE('',*,*,#7783,.T.);
#11344=ORIENTED_EDGE('',*,*,#7841,.T.);
#11345=ORIENTED_EDGE('',*,*,#7632,.T.);
#11346=ORIENTED_EDGE('',*,*,#7838,.F.);
#11347=ORIENTED_EDGE('',*,*,#7785,.T.);
#11348=ORIENTED_EDGE('',*,*,#7839,.F.);
#11349=ORIENTED_EDGE('',*,*,#7630,.T.);
#11350=ORIENTED_EDGE('',*,*,#7840,.T.);
#11351=ORIENTED_EDGE('',*,*,#7762,.T.);
#11352=ORIENTED_EDGE('',*,*,#7842,.F.);
#11353=ORIENTED_EDGE('',*,*,#7757,.F.);
#11354=ORIENTED_EDGE('',*,*,#7843,.F.);
#11355=ORIENTED_EDGE('',*,*,#7844,.T.);
#11356=ORIENTED_EDGE('',*,*,#7755,.T.);
#11357=ORIENTED_EDGE('',*,*,#7759,.T.);
#11358=ORIENTED_EDGE('',*,*,#7845,.T.);
#11359=ORIENTED_EDGE('',*,*,#7760,.F.);
#11360=ORIENTED_EDGE('',*,*,#7753,.F.);
#11361=ORIENTED_EDGE('',*,*,#7845,.F.);
#11362=ORIENTED_EDGE('',*,*,#7758,.T.);
#11363=ORIENTED_EDGE('',*,*,#7842,.T.);
#11364=ORIENTED_EDGE('',*,*,#7761,.F.);
#11365=ORIENTED_EDGE('',*,*,#7843,.T.);
#11366=ORIENTED_EDGE('',*,*,#7756,.T.);
#11367=ORIENTED_EDGE('',*,*,#7844,.F.);
#11368=ORIENTED_EDGE('',*,*,#7763,.F.);
#12219=CYLINDRICAL_SURFACE('',#14271,7.5);
#12220=CYLINDRICAL_SURFACE('',#14274,12.4653846153846);
#12221=CYLINDRICAL_SURFACE('',#14276,12.4653846153846);
#12222=CYLINDRICAL_SURFACE('',#14312,17.6897435897436);
#12223=CYLINDRICAL_SURFACE('',#14315,16.2686153846154);
#12224=CYLINDRICAL_SURFACE('',#14317,16.0346153846154);
#12225=CYLINDRICAL_SURFACE('',#14322,16.0346153846154);
#12226=CYLINDRICAL_SURFACE('',#14323,16.2686153846154);
#12227=CYLINDRICAL_SURFACE('',#14325,17.6897435897436);
#12228=CYLINDRICAL_SURFACE('',#14335,21.);
#12229=CYLINDRICAL_SURFACE('',#14440,14.25);
#12230=CYLINDRICAL_SURFACE('',#14443,15.1423076923077);
#12231=CYLINDRICAL_SURFACE('',#14456,15.1423076923077);
#12232=CYLINDRICAL_SURFACE('',#14457,14.25);
#12233=CYLINDRICAL_SURFACE('',#14466,15.1423076923077);
#12234=CYLINDRICAL_SURFACE('',#14467,14.25);
#12235=CYLINDRICAL_SURFACE('',#14468,14.25);
#12236=CYLINDRICAL_SURFACE('',#14471,15.1423076923077);
#12237=CYLINDRICAL_SURFACE('',#14484,15.1423076923077);
#12238=CYLINDRICAL_SURFACE('',#14485,14.25);
#12239=CYLINDRICAL_SURFACE('',#14486,14.25);
#12240=CYLINDRICAL_SURFACE('',#14489,15.1423076923077);
#12241=CYLINDRICAL_SURFACE('',#14502,15.1423076923077);
#12242=CYLINDRICAL_SURFACE('',#14503,14.25);
#12243=CYLINDRICAL_SURFACE('',#14504,14.25);
#12244=CYLINDRICAL_SURFACE('',#14507,15.1423076923077);
#12245=CYLINDRICAL_SURFACE('',#14520,15.1423076923077);
#12246=CYLINDRICAL_SURFACE('',#14521,14.25);
#12247=CYLINDRICAL_SURFACE('',#14522,14.25);
#12248=CYLINDRICAL_SURFACE('',#14525,15.1423076923077);
#12249=CYLINDRICAL_SURFACE('',#14538,15.1423076923077);
#12250=CYLINDRICAL_SURFACE('',#14539,14.25);
#12251=CYLINDRICAL_SURFACE('',#14540,14.25);
#12252=CYLINDRICAL_SURFACE('',#14543,15.1423076923077);
#12253=CYLINDRICAL_SURFACE('',#14556,15.1423076923077);
#12254=CYLINDRICAL_SURFACE('',#14557,14.25);
#12255=CYLINDRICAL_SURFACE('',#14564,15.1423076923077);
#12256=CYLINDRICAL_SURFACE('',#14565,14.25);
#12793=ADVANCED_FACE('',(#1781),#145,.F.);
#12794=ADVANCED_FACE('',(#1782),#146,.T.);
#12795=ADVANCED_FACE('',(#1783),#147,.T.);
#12796=ADVANCED_FACE('',(#1784),#107,.F.);
#12797=ADVANCED_FACE('',(#1785),#12219,.F.);
#12798=ADVANCED_FACE('',(#1786),#108,.F.);
#12799=ADVANCED_FACE('',(#1787),#12220,.T.);
#12800=ADVANCED_FACE('',(#1788),#12221,.T.);
#12801=ADVANCED_FACE('',(#1789,#383),#1175,.T.);
#12802=ADVANCED_FACE('',(#1790,#384),#1176,.T.);
#12803=ADVANCED_FACE('',(#1791),#71,.T.);
#12804=ADVANCED_FACE('',(#1792),#72,.T.);
#12805=ADVANCED_FACE('',(#1793),#73,.T.);
#12806=ADVANCED_FACE('',(#1794),#74,.T.);
#12807=ADVANCED_FACE('',(#1795),#75,.T.);
#12808=ADVANCED_FACE('',(#1796),#76,.T.);
#12809=ADVANCED_FACE('',(#1797),#77,.T.);
#12810=ADVANCED_FACE('',(#1798),#148,.T.);
#12811=ADVANCED_FACE('',(#1799),#149,.T.);
#12812=ADVANCED_FACE('',(#1800),#150,.T.);
#12813=ADVANCED_FACE('',(#1801),#151,.T.);
#12814=ADVANCED_FACE('',(#1802),#12222,.F.);
#12815=ADVANCED_FACE('',(#1803),#12223,.F.);
#12816=ADVANCED_FACE('',(#1804),#12224,.F.);
#12817=ADVANCED_FACE('',(#1805),#152,.F.);
#12818=ADVANCED_FACE('',(#1806),#12225,.F.);
#12819=ADVANCED_FACE('',(#1807),#12226,.F.);
#12820=ADVANCED_FACE('',(#1808),#12227,.F.);
#12821=ADVANCED_FACE('',(#1809),#109,.T.);
#12822=ADVANCED_FACE('',(#1810),#110,.T.);
#12823=ADVANCED_FACE('',(#1811),#12228,.T.);
#12824=ADVANCED_FACE('',(#1812,#385),#1177,.T.);
#12825=ADVANCED_FACE('',(#1813,#386),#1178,.T.);
#12826=ADVANCED_FACE('',(#1814,#387),#1179,.F.);
#12827=ADVANCED_FACE('',(#1815,#388),#1180,.F.);
#12828=ADVANCED_FACE('',(#1816,#389),#1181,.F.);
#12829=ADVANCED_FACE('',(#1817,#390),#1182,.F.);
#12830=ADVANCED_FACE('',(#1818,#391,#392),#153,.T.);
#12831=ADVANCED_FACE('',(#1819,#393,#394),#78,.F.);
#12832=ADVANCED_FACE('',(#1820,#395,#396),#154,.T.);
#12833=ADVANCED_FACE('',(#1821,#397,#398),#79,.F.);
#12834=ADVANCED_FACE('',(#1822,#399,#400),#155,.T.);
#12835=ADVANCED_FACE('',(#1823,#401,#402),#80,.F.);
#12836=ADVANCED_FACE('',(#1824,#403,#404),#156,.T.);
#12837=ADVANCED_FACE('',(#1825,#405,#406),#81,.F.);
#12838=ADVANCED_FACE('',(#1826,#407,#408),#157,.T.);
#12839=ADVANCED_FACE('',(#1827,#409,#410),#82,.F.);
#12840=ADVANCED_FACE('',(#1828,#411,#412),#158,.T.);
#12841=ADVANCED_FACE('',(#1829,#413,#414),#83,.F.);
#12842=ADVANCED_FACE('',(#1830,#415,#416),#84,.F.);
#12843=ADVANCED_FACE('',(#1831,#417,#418),#159,.T.);
#12844=ADVANCED_FACE('',(#1832),#12229,.F.);
#12845=ADVANCED_FACE('',(#1833),#12230,.T.);
#12846=ADVANCED_FACE('',(#1834),#1183,.F.);
#12847=ADVANCED_FACE('',(#1835),#1184,.T.);
#12848=ADVANCED_FACE('',(#1836,#419),#1185,.F.);
#12849=ADVANCED_FACE('',(#1837,#420),#1186,.F.);
#12850=ADVANCED_FACE('',(#1838),#1187,.F.);
#12851=ADVANCED_FACE('',(#1839),#1188,.T.);
#12852=ADVANCED_FACE('',(#1840),#12231,.T.);
#12853=ADVANCED_FACE('',(#1841),#12232,.F.);
#12854=ADVANCED_FACE('',(#1842,#421),#1189,.F.);
#12855=ADVANCED_FACE('',(#1843,#422),#1190,.F.);
#12856=ADVANCED_FACE('',(#1844),#1191,.T.);
#12857=ADVANCED_FACE('',(#1845),#1192,.F.);
#12858=ADVANCED_FACE('',(#1846),#12233,.T.);
#12859=ADVANCED_FACE('',(#1847),#12234,.F.);
#12860=ADVANCED_FACE('',(#1848),#12235,.F.);
#12861=ADVANCED_FACE('',(#1849),#12236,.T.);
#12862=ADVANCED_FACE('',(#1850),#1193,.T.);
#12863=ADVANCED_FACE('',(#1851),#1194,.F.);
#12864=ADVANCED_FACE('',(#1852,#423),#1195,.F.);
#12865=ADVANCED_FACE('',(#1853,#424),#1196,.F.);
#12866=ADVANCED_FACE('',(#1854),#1197,.T.);
#12867=ADVANCED_FACE('',(#1855),#1198,.F.);
#12868=ADVANCED_FACE('',(#1856),#12237,.T.);
#12869=ADVANCED_FACE('',(#1857),#12238,.F.);
#12870=ADVANCED_FACE('',(#1858),#12239,.F.);
#12871=ADVANCED_FACE('',(#1859),#12240,.T.);
#12872=ADVANCED_FACE('',(#1860),#1199,.T.);
#12873=ADVANCED_FACE('',(#1861),#1200,.F.);
#12874=ADVANCED_FACE('',(#1862,#425),#1201,.F.);
#12875=ADVANCED_FACE('',(#1863,#426),#1202,.F.);
#12876=ADVANCED_FACE('',(#1864),#1203,.T.);
#12877=ADVANCED_FACE('',(#1865),#1204,.F.);
#12878=ADVANCED_FACE('',(#1866),#12241,.T.);
#12879=ADVANCED_FACE('',(#1867),#12242,.F.);
#12880=ADVANCED_FACE('',(#1868),#12243,.F.);
#12881=ADVANCED_FACE('',(#1869),#12244,.T.);
#12882=ADVANCED_FACE('',(#1870),#1205,.T.);
#12883=ADVANCED_FACE('',(#1871),#1206,.F.);
#12884=ADVANCED_FACE('',(#1872,#427),#1207,.F.);
#12885=ADVANCED_FACE('',(#1873,#428),#1208,.F.);
#12886=ADVANCED_FACE('',(#1874),#1209,.T.);
#12887=ADVANCED_FACE('',(#1875),#1210,.F.);
#12888=ADVANCED_FACE('',(#1876),#12245,.T.);
#12889=ADVANCED_FACE('',(#1877),#12246,.F.);
#12890=ADVANCED_FACE('',(#1878),#12247,.F.);
#12891=ADVANCED_FACE('',(#1879),#12248,.T.);
#12892=ADVANCED_FACE('',(#1880),#1211,.T.);
#12893=ADVANCED_FACE('',(#1881),#1212,.F.);
#12894=ADVANCED_FACE('',(#1882,#429),#1213,.F.);
#12895=ADVANCED_FACE('',(#1883,#430),#1214,.F.);
#12896=ADVANCED_FACE('',(#1884),#1215,.T.);
#12897=ADVANCED_FACE('',(#1885),#1216,.F.);
#12898=ADVANCED_FACE('',(#1886),#12249,.T.);
#12899=ADVANCED_FACE('',(#1887),#12250,.F.);
#12900=ADVANCED_FACE('',(#1888),#12251,.F.);
#12901=ADVANCED_FACE('',(#1889),#12252,.T.);
#12902=ADVANCED_FACE('',(#1890),#1217,.T.);
#12903=ADVANCED_FACE('',(#1891),#1218,.F.);
#12904=ADVANCED_FACE('',(#1892,#431),#1219,.F.);
#12905=ADVANCED_FACE('',(#1893,#432),#1220,.F.);
#12906=ADVANCED_FACE('',(#1894),#1221,.T.);
#12907=ADVANCED_FACE('',(#1895),#1222,.F.);
#12908=ADVANCED_FACE('',(#1896),#12253,.T.);
#12909=ADVANCED_FACE('',(#1897),#12254,.F.);
#12910=ADVANCED_FACE('',(#1898),#1223,.F.);
#12911=ADVANCED_FACE('',(#1899),#1224,.T.);
#12912=ADVANCED_FACE('',(#1900),#12255,.T.);
#12913=ADVANCED_FACE('',(#1901),#12256,.F.);
#13073=CLOSED_SHELL('',(#12793,#12794,#12795,#12796,#12797,#12798,#12799,
#12800,#12801,#12802));
#13074=CLOSED_SHELL('',(#12803));
#13075=CLOSED_SHELL('',(#12804));
#13076=CLOSED_SHELL('',(#12805));
#13077=CLOSED_SHELL('',(#12806));
#13078=CLOSED_SHELL('',(#12807));
#13079=CLOSED_SHELL('',(#12808));
#13080=CLOSED_SHELL('',(#12809));
#13081=CLOSED_SHELL('',(#12810,#12811,#12812,#12813,#12814,#12815,#12816,
#12817,#12818,#12819,#12820,#12821,#12822,#12823,#12824,#12825,#12826,#12827,
#12828,#12829));
#13082=CLOSED_SHELL('',(#12830,#12831,#12832,#12833,#12834,#12835,#12836,
#12837,#12838,#12839,#12840,#12841,#12842,#12843,#12844,#12845,#12846,#12847,
#12848,#12849,#12850,#12851,#12852,#12853,#12854,#12855,#12856,#12857,#12858,
#12859,#12860,#12861,#12862,#12863,#12864,#12865,#12866,#12867,#12868,#12869,
#12870,#12871,#12872,#12873,#12874,#12875,#12876,#12877,#12878,#12879,#12880,
#12881,#12882,#12883,#12884,#12885,#12886,#12887,#12888,#12889,#12890,#12891,
#12892,#12893,#12894,#12895,#12896,#12897,#12898,#12899,#12900,#12901,#12902,
#12903,#12904,#12905,#12906,#12907,#12908,#12909,#12910,#12911,#12912,#12913));
#14253=AXIS2_PLACEMENT_3D('',#40850,#17443,#17444);
#14254=AXIS2_PLACEMENT_3D('',#40851,#17445,#17446);
#14255=AXIS2_PLACEMENT_3D('',#40853,#17447,#17448);
#14256=AXIS2_PLACEMENT_3D('',#40855,#17449,#17450);
#14257=AXIS2_PLACEMENT_3D('',#40856,#17451,#17452);
#14258=AXIS2_PLACEMENT_3D('',#40857,#17453,#17454);
#14259=AXIS2_PLACEMENT_3D('',#40860,#17455,#17456);
#14260=AXIS2_PLACEMENT_3D('',#40862,#17457,#17458);
#14261=AXIS2_PLACEMENT_3D('',#40864,#17459,#17460);
#14262=AXIS2_PLACEMENT_3D('',#40865,#17461,#17462);
#14263=AXIS2_PLACEMENT_3D('',#40866,#17463,#17464);
#14264=AXIS2_PLACEMENT_3D('',#40867,#17465,#17466);
#14265=AXIS2_PLACEMENT_3D('',#40870,#17467,#17468);
#14266=AXIS2_PLACEMENT_3D('',#40872,#17469,#17470);
#14267=AXIS2_PLACEMENT_3D('',#40873,#17471,#17472);
#14268=AXIS2_PLACEMENT_3D('',#40874,#17473,#17474);
#14269=AXIS2_PLACEMENT_3D('',#40875,#17475,#17476);
#14270=AXIS2_PLACEMENT_3D('',#40878,#17478,#17479);
#14271=AXIS2_PLACEMENT_3D('',#40879,#17480,#17481);
#14272=AXIS2_PLACEMENT_3D('',#40881,#17483,#17484);
#14273=AXIS2_PLACEMENT_3D('',#40884,#17486,#17487);
#14274=AXIS2_PLACEMENT_3D('',#40885,#17488,#17489);
#14275=AXIS2_PLACEMENT_3D('',#40887,#17490,#17491);
#14276=AXIS2_PLACEMENT_3D('',#40889,#17493,#17494);
#14277=AXIS2_PLACEMENT_3D('',#40892,#17496,#17497);
#14278=AXIS2_PLACEMENT_3D('',#40893,#17498,#17499);
#14279=AXIS2_PLACEMENT_3D('',#40894,#17500,#17501);
#14280=AXIS2_PLACEMENT_3D('',#40895,#17502,#17503);
#14281=AXIS2_PLACEMENT_3D('',#40898,#17504,#17505);
#14282=AXIS2_PLACEMENT_3D('',#40899,#17506,#17507);
#14283=AXIS2_PLACEMENT_3D('',#40902,#17508,#17509);
#14284=AXIS2_PLACEMENT_3D('',#40903,#17510,#17511);
#14285=AXIS2_PLACEMENT_3D('',#40906,#17512,#17513);
#14286=AXIS2_PLACEMENT_3D('',#40907,#17514,#17515);
#14287=AXIS2_PLACEMENT_3D('',#40910,#17516,#17517);
#14288=AXIS2_PLACEMENT_3D('',#40911,#17518,#17519);
#14289=AXIS2_PLACEMENT_3D('',#40914,#17520,#17521);
#14290=AXIS2_PLACEMENT_3D('',#40915,#17522,#17523);
#14291=AXIS2_PLACEMENT_3D('',#40918,#17524,#17525);
#14292=AXIS2_PLACEMENT_3D('',#40919,#17526,#17527);
#14293=AXIS2_PLACEMENT_3D('',#40922,#17528,#17529);
#14294=AXIS2_PLACEMENT_3D('',#40923,#17530,#17531);
#14295=AXIS2_PLACEMENT_3D('',#40925,#17532,#17533);
#14296=AXIS2_PLACEMENT_3D('',#40927,#17534,#17535);
#14297=AXIS2_PLACEMENT_3D('',#40929,#17536,#17537);
#14298=AXIS2_PLACEMENT_3D('',#40930,#17538,#17539);
#14299=AXIS2_PLACEMENT_3D('',#40931,#17540,#17541);
#14300=AXIS2_PLACEMENT_3D('',#40933,#17542,#17543);
#14301=AXIS2_PLACEMENT_3D('',#40935,#17544,#17545);
#14302=AXIS2_PLACEMENT_3D('',#40936,#17546,#17547);
#14303=AXIS2_PLACEMENT_3D('',#40937,#17548,#17549);
#14304=AXIS2_PLACEMENT_3D('',#40939,#17550,#17551);
#14305=AXIS2_PLACEMENT_3D('',#40941,#17552,#17553);
#14306=AXIS2_PLACEMENT_3D('',#40942,#17554,#17555);
#14307=AXIS2_PLACEMENT_3D('',#40943,#17556,#17557);
#14308=AXIS2_PLACEMENT_3D('',#40946,#17558,#17559);
#14309=AXIS2_PLACEMENT_3D('',#40948,#17560,#17561);
#14310=AXIS2_PLACEMENT_3D('',#40949,#17562,#17563);
#14311=AXIS2_PLACEMENT_3D('',#40950,#17564,#17565);
#14312=AXIS2_PLACEMENT_3D('',#40951,#17566,#17567);
#14313=AXIS2_PLACEMENT_3D('',#40953,#17568,#17569);
#14314=AXIS2_PLACEMENT_3D('',#40956,#17571,#17572);
#14315=AXIS2_PLACEMENT_3D('',#40957,#17573,#17574);
#14316=AXIS2_PLACEMENT_3D('',#40960,#17576,#17577);
#14317=AXIS2_PLACEMENT_3D('',#40961,#17578,#17579);
#14318=AXIS2_PLACEMENT_3D('',#40963,#17580,#17581);
#14319=AXIS2_PLACEMENT_3D('',#40965,#17583,#17584);
#14320=AXIS2_PLACEMENT_3D('',#40967,#17585,#17586);
#14321=AXIS2_PLACEMENT_3D('',#40968,#17587,#17588);
#14322=AXIS2_PLACEMENT_3D('',#40969,#17589,#17590);
#14323=AXIS2_PLACEMENT_3D('',#40971,#17592,#17593);
#14324=AXIS2_PLACEMENT_3D('',#40973,#17594,#17595);
#14325=AXIS2_PLACEMENT_3D('',#40975,#17597,#17598);
#14326=AXIS2_PLACEMENT_3D('',#40977,#17599,#17600);
#14327=AXIS2_PLACEMENT_3D('',#40980,#17602,#17603);
#14328=AXIS2_PLACEMENT_3D('',#40981,#17604,#17605);
#14329=AXIS2_PLACEMENT_3D('',#40983,#17606,#17607);
#14330=AXIS2_PLACEMENT_3D('',#40986,#17609,#17610);
#14331=AXIS2_PLACEMENT_3D('',#40987,#17611,#17612);
#14332=AXIS2_PLACEMENT_3D('',#40990,#17613,#17614);
#14333=AXIS2_PLACEMENT_3D('',#40991,#17615,#17616);
#14334=AXIS2_PLACEMENT_3D('',#40994,#17618,#17619);
#14335=AXIS2_PLACEMENT_3D('',#40995,#17620,#17621);
#14336=AXIS2_PLACEMENT_3D('',#40997,#17623,#17624);
#14337=AXIS2_PLACEMENT_3D('',#40998,#17625,#17626);
#14338=AXIS2_PLACEMENT_3D('',#40999,#17627,#17628);
#14339=AXIS2_PLACEMENT_3D('',#41000,#17629,#17630);
#14340=AXIS2_PLACEMENT_3D('',#41001,#17631,#17632);
#14341=AXIS2_PLACEMENT_3D('',#41002,#17633,#17634);
#14342=AXIS2_PLACEMENT_3D('',#41003,#17635,#17636);
#14343=AXIS2_PLACEMENT_3D('',#41005,#17637,#17638);
#14344=AXIS2_PLACEMENT_3D('',#41007,#17639,#17640);
#14345=AXIS2_PLACEMENT_3D('',#41008,#17641,#17642);
#14346=AXIS2_PLACEMENT_3D('',#41117,#17643,#17644);
#14347=AXIS2_PLACEMENT_3D('',#41120,#17645,#17646);
#14348=AXIS2_PLACEMENT_3D('',#41129,#17647,#17648);
#14349=AXIS2_PLACEMENT_3D('',#41137,#17649,#17650);
#14350=AXIS2_PLACEMENT_3D('',#41139,#17651,#17652);
#14351=AXIS2_PLACEMENT_3D('',#41141,#17653,#17654);
#14352=AXIS2_PLACEMENT_3D('',#41151,#17655,#17656);
#14353=AXIS2_PLACEMENT_3D('',#41160,#17657,#17658);
#14354=AXIS2_PLACEMENT_3D('',#41162,#17659,#17660);
#14355=AXIS2_PLACEMENT_3D('',#41164,#17661,#17662);
#14356=AXIS2_PLACEMENT_3D('',#41165,#17663,#17664);
#14357=AXIS2_PLACEMENT_3D('',#41167,#17665,#17666);
#14358=AXIS2_PLACEMENT_3D('',#41169,#17667,#17668);
#14359=AXIS2_PLACEMENT_3D('',#41170,#17669,#17670);
#14360=AXIS2_PLACEMENT_3D('',#41279,#17671,#17672);
#14361=AXIS2_PLACEMENT_3D('',#41282,#17673,#17674);
#14362=AXIS2_PLACEMENT_3D('',#41291,#17675,#17676);
#14363=AXIS2_PLACEMENT_3D('',#41299,#17677,#17678);
#14364=AXIS2_PLACEMENT_3D('',#41301,#17679,#17680);
#14365=AXIS2_PLACEMENT_3D('',#41303,#17681,#17682);
#14366=AXIS2_PLACEMENT_3D('',#41313,#17683,#17684);
#14367=AXIS2_PLACEMENT_3D('',#41322,#17685,#17686);
#14368=AXIS2_PLACEMENT_3D('',#41324,#17687,#17688);
#14369=AXIS2_PLACEMENT_3D('',#41326,#17689,#17690);
#14370=AXIS2_PLACEMENT_3D('',#41327,#17691,#17692);
#14371=AXIS2_PLACEMENT_3D('',#41329,#17693,#17694);
#14372=AXIS2_PLACEMENT_3D('',#41331,#17695,#17696);
#14373=AXIS2_PLACEMENT_3D('',#41332,#17697,#17698);
#14374=AXIS2_PLACEMENT_3D('',#41441,#17699,#17700);
#14375=AXIS2_PLACEMENT_3D('',#41444,#17701,#17702);
#14376=AXIS2_PLACEMENT_3D('',#41453,#17703,#17704);
#14377=AXIS2_PLACEMENT_3D('',#41461,#17705,#17706);
#14378=AXIS2_PLACEMENT_3D('',#41463,#17707,#17708);
#14379=AXIS2_PLACEMENT_3D('',#41465,#17709,#17710);
#14380=AXIS2_PLACEMENT_3D('',#41475,#17711,#17712);
#14381=AXIS2_PLACEMENT_3D('',#41484,#17713,#17714);
#14382=AXIS2_PLACEMENT_3D('',#41486,#17715,#17716);
#14383=AXIS2_PLACEMENT_3D('',#41488,#17717,#17718);
#14384=AXIS2_PLACEMENT_3D('',#41489,#17719,#17720);
#14385=AXIS2_PLACEMENT_3D('',#41491,#17721,#17722);
#14386=AXIS2_PLACEMENT_3D('',#41493,#17723,#17724);
#14387=AXIS2_PLACEMENT_3D('',#41494,#17725,#17726);
#14388=AXIS2_PLACEMENT_3D('',#41603,#17727,#17728);
#14389=AXIS2_PLACEMENT_3D('',#41606,#17729,#17730);
#14390=AXIS2_PLACEMENT_3D('',#41615,#17731,#17732);
#14391=AXIS2_PLACEMENT_3D('',#41623,#17733,#17734);
#14392=AXIS2_PLACEMENT_3D('',#41625,#17735,#17736);
#14393=AXIS2_PLACEMENT_3D('',#41627,#17737,#17738);
#14394=AXIS2_PLACEMENT_3D('',#41637,#17739,#17740);
#14395=AXIS2_PLACEMENT_3D('',#41646,#17741,#17742);
#14396=AXIS2_PLACEMENT_3D('',#41648,#17743,#17744);
#14397=AXIS2_PLACEMENT_3D('',#41650,#17745,#17746);
#14398=AXIS2_PLACEMENT_3D('',#41651,#17747,#17748);
#14399=AXIS2_PLACEMENT_3D('',#41653,#17749,#17750);
#14400=AXIS2_PLACEMENT_3D('',#41655,#17751,#17752);
#14401=AXIS2_PLACEMENT_3D('',#41656,#17753,#17754);
#14402=AXIS2_PLACEMENT_3D('',#41765,#17755,#17756);
#14403=AXIS2_PLACEMENT_3D('',#41768,#17757,#17758);
#14404=AXIS2_PLACEMENT_3D('',#41777,#17759,#17760);
#14405=AXIS2_PLACEMENT_3D('',#41785,#17761,#17762);
#14406=AXIS2_PLACEMENT_3D('',#41787,#17763,#17764);
#14407=AXIS2_PLACEMENT_3D('',#41789,#17765,#17766);
#14408=AXIS2_PLACEMENT_3D('',#41799,#17767,#17768);
#14409=AXIS2_PLACEMENT_3D('',#41808,#17769,#17770);
#14410=AXIS2_PLACEMENT_3D('',#41810,#17771,#17772);
#14411=AXIS2_PLACEMENT_3D('',#41812,#17773,#17774);
#14412=AXIS2_PLACEMENT_3D('',#41813,#17775,#17776);
#14413=AXIS2_PLACEMENT_3D('',#41815,#17777,#17778);
#14414=AXIS2_PLACEMENT_3D('',#41817,#17779,#17780);
#14415=AXIS2_PLACEMENT_3D('',#41818,#17781,#17782);
#14416=AXIS2_PLACEMENT_3D('',#41927,#17783,#17784);
#14417=AXIS2_PLACEMENT_3D('',#41930,#17785,#17786);
#14418=AXIS2_PLACEMENT_3D('',#41932,#17787,#17788);
#14419=AXIS2_PLACEMENT_3D('',#41934,#17789,#17790);
#14420=AXIS2_PLACEMENT_3D('',#41944,#17791,#17792);
#14421=AXIS2_PLACEMENT_3D('',#41953,#17793,#17794);
#14422=AXIS2_PLACEMENT_3D('',#41955,#17795,#17796);
#14423=AXIS2_PLACEMENT_3D('',#41964,#17797,#17798);
#14424=AXIS2_PLACEMENT_3D('',#41972,#17799,#17800);
#14425=AXIS2_PLACEMENT_3D('',#41974,#17801,#17802);
#14426=AXIS2_PLACEMENT_3D('',#41975,#17803,#17804);
#14427=AXIS2_PLACEMENT_3D('',#41978,#17805,#17806);
#14428=AXIS2_PLACEMENT_3D('',#41987,#17807,#17808);
#14429=AXIS2_PLACEMENT_3D('',#41995,#17809,#17810);
#14430=AXIS2_PLACEMENT_3D('',#41997,#17811,#17812);
#14431=AXIS2_PLACEMENT_3D('',#41999,#17813,#17814);
#14432=AXIS2_PLACEMENT_3D('',#42009,#17815,#17816);
#14433=AXIS2_PLACEMENT_3D('',#42018,#17817,#17818);
#14434=AXIS2_PLACEMENT_3D('',#42020,#17819,#17820);
#14435=AXIS2_PLACEMENT_3D('',#42022,#17821,#17822);
#14436=AXIS2_PLACEMENT_3D('',#42023,#17823,#17824);
#14437=AXIS2_PLACEMENT_3D('',#42025,#17825,#17826);
#14438=AXIS2_PLACEMENT_3D('',#42027,#17827,#17828);
#14439=AXIS2_PLACEMENT_3D('',#42028,#17829,#17830);
#14440=AXIS2_PLACEMENT_3D('',#42137,#17831,#17832);
#14441=AXIS2_PLACEMENT_3D('',#42138,#17833,#17834);
#14442=AXIS2_PLACEMENT_3D('',#42139,#17835,#17836);
#14443=AXIS2_PLACEMENT_3D('',#42140,#17837,#17838);
#14444=AXIS2_PLACEMENT_3D('',#42141,#17839,#17840);
#14445=AXIS2_PLACEMENT_3D('',#42142,#17841,#17842);
#14446=AXIS2_PLACEMENT_3D('',#42143,#17843,#17844);
#14447=AXIS2_PLACEMENT_3D('',#42144,#17845,#17846);
#14448=AXIS2_PLACEMENT_3D('',#42145,#17847,#17848);
#14449=AXIS2_PLACEMENT_3D('',#42146,#17849,#17850);
#14450=AXIS2_PLACEMENT_3D('',#42147,#17851,#17852);
#14451=AXIS2_PLACEMENT_3D('',#42148,#17853,#17854);
#14452=AXIS2_PLACEMENT_3D('',#42149,#17855,#17856);
#14453=AXIS2_PLACEMENT_3D('',#42150,#17857,#17858);
#14454=AXIS2_PLACEMENT_3D('',#42151,#17859,#17860);
#14455=AXIS2_PLACEMENT_3D('',#42152,#17861,#17862);
#14456=AXIS2_PLACEMENT_3D('',#42153,#17863,#17864);
#14457=AXIS2_PLACEMENT_3D('',#42154,#17865,#17866);
#14458=AXIS2_PLACEMENT_3D('',#42155,#17867,#17868);
#14459=AXIS2_PLACEMENT_3D('',#42156,#17869,#17870);
#14460=AXIS2_PLACEMENT_3D('',#42157,#17871,#17872);
#14461=AXIS2_PLACEMENT_3D('',#42158,#17873,#17874);
#14462=AXIS2_PLACEMENT_3D('',#42159,#17875,#17876);
#14463=AXIS2_PLACEMENT_3D('',#42160,#17877,#17878);
#14464=AXIS2_PLACEMENT_3D('',#42161,#17879,#17880);
#14465=AXIS2_PLACEMENT_3D('',#42162,#17881,#17882);
#14466=AXIS2_PLACEMENT_3D('',#42163,#17883,#17884);
#14467=AXIS2_PLACEMENT_3D('',#42164,#17885,#17886);
#14468=AXIS2_PLACEMENT_3D('',#42165,#17887,#17888);
#14469=AXIS2_PLACEMENT_3D('',#42166,#17889,#17890);
#14470=AXIS2_PLACEMENT_3D('',#42167,#17891,#17892);
#14471=AXIS2_PLACEMENT_3D('',#42168,#17893,#17894);
#14472=AXIS2_PLACEMENT_3D('',#42169,#17895,#17896);
#14473=AXIS2_PLACEMENT_3D('',#42170,#17897,#17898);
#14474=AXIS2_PLACEMENT_3D('',#42171,#17899,#17900);
#14475=AXIS2_PLACEMENT_3D('',#42172,#17901,#17902);
#14476=AXIS2_PLACEMENT_3D('',#42173,#17903,#17904);
#14477=AXIS2_PLACEMENT_3D('',#42174,#17905,#17906);
#14478=AXIS2_PLACEMENT_3D('',#42175,#17907,#17908);
#14479=AXIS2_PLACEMENT_3D('',#42176,#17909,#17910);
#14480=AXIS2_PLACEMENT_3D('',#42177,#17911,#17912);
#14481=AXIS2_PLACEMENT_3D('',#42178,#17913,#17914);
#14482=AXIS2_PLACEMENT_3D('',#42179,#17915,#17916);
#14483=AXIS2_PLACEMENT_3D('',#42180,#17917,#17918);
#14484=AXIS2_PLACEMENT_3D('',#42181,#17919,#17920);
#14485=AXIS2_PLACEMENT_3D('',#42182,#17921,#17922);
#14486=AXIS2_PLACEMENT_3D('',#42183,#17923,#17924);
#14487=AXIS2_PLACEMENT_3D('',#42184,#17925,#17926);
#14488=AXIS2_PLACEMENT_3D('',#42185,#17927,#17928);
#14489=AXIS2_PLACEMENT_3D('',#42186,#17929,#17930);
#14490=AXIS2_PLACEMENT_3D('',#42187,#17931,#17932);
#14491=AXIS2_PLACEMENT_3D('',#42188,#17933,#17934);
#14492=AXIS2_PLACEMENT_3D('',#42189,#17935,#17936);
#14493=AXIS2_PLACEMENT_3D('',#42190,#17937,#17938);
#14494=AXIS2_PLACEMENT_3D('',#42191,#17939,#17940);
#14495=AXIS2_PLACEMENT_3D('',#42192,#17941,#17942);
#14496=AXIS2_PLACEMENT_3D('',#42193,#17943,#17944);
#14497=AXIS2_PLACEMENT_3D('',#42194,#17945,#17946);
#14498=AXIS2_PLACEMENT_3D('',#42195,#17947,#17948);
#14499=AXIS2_PLACEMENT_3D('',#42196,#17949,#17950);
#14500=AXIS2_PLACEMENT_3D('',#42197,#17951,#17952);
#14501=AXIS2_PLACEMENT_3D('',#42198,#17953,#17954);
#14502=AXIS2_PLACEMENT_3D('',#42199,#17955,#17956);
#14503=AXIS2_PLACEMENT_3D('',#42200,#17957,#17958);
#14504=AXIS2_PLACEMENT_3D('',#42201,#17959,#17960);
#14505=AXIS2_PLACEMENT_3D('',#42202,#17961,#17962);
#14506=AXIS2_PLACEMENT_3D('',#42203,#17963,#17964);
#14507=AXIS2_PLACEMENT_3D('',#42204,#17965,#17966);
#14508=AXIS2_PLACEMENT_3D('',#42205,#17967,#17968);
#14509=AXIS2_PLACEMENT_3D('',#42206,#17969,#17970);
#14510=AXIS2_PLACEMENT_3D('',#42207,#17971,#17972);
#14511=AXIS2_PLACEMENT_3D('',#42208,#17973,#17974);
#14512=AXIS2_PLACEMENT_3D('',#42209,#17975,#17976);
#14513=AXIS2_PLACEMENT_3D('',#42210,#17977,#17978);
#14514=AXIS2_PLACEMENT_3D('',#42211,#17979,#17980);
#14515=AXIS2_PLACEMENT_3D('',#42212,#17981,#17982);
#14516=AXIS2_PLACEMENT_3D('',#42213,#17983,#17984);
#14517=AXIS2_PLACEMENT_3D('',#42214,#17985,#17986);
#14518=AXIS2_PLACEMENT_3D('',#42215,#17987,#17988);
#14519=AXIS2_PLACEMENT_3D('',#42216,#17989,#17990);
#14520=AXIS2_PLACEMENT_3D('',#42217,#17991,#17992);
#14521=AXIS2_PLACEMENT_3D('',#42218,#17993,#17994);
#14522=AXIS2_PLACEMENT_3D('',#42219,#17995,#17996);
#14523=AXIS2_PLACEMENT_3D('',#42220,#17997,#17998);
#14524=AXIS2_PLACEMENT_3D('',#42221,#17999,#18000);
#14525=AXIS2_PLACEMENT_3D('',#42222,#18001,#18002);
#14526=AXIS2_PLACEMENT_3D('',#42223,#18003,#18004);
#14527=AXIS2_PLACEMENT_3D('',#42224,#18005,#18006);
#14528=AXIS2_PLACEMENT_3D('',#42225,#18007,#18008);
#14529=AXIS2_PLACEMENT_3D('',#42226,#18009,#18010);
#14530=AXIS2_PLACEMENT_3D('',#42227,#18011,#18012);
#14531=AXIS2_PLACEMENT_3D('',#42228,#18013,#18014);
#14532=AXIS2_PLACEMENT_3D('',#42229,#18015,#18016);
#14533=AXIS2_PLACEMENT_3D('',#42230,#18017,#18018);
#14534=AXIS2_PLACEMENT_3D('',#42231,#18019,#18020);
#14535=AXIS2_PLACEMENT_3D('',#42232,#18021,#18022);
#14536=AXIS2_PLACEMENT_3D('',#42233,#18023,#18024);
#14537=AXIS2_PLACEMENT_3D('',#42234,#18025,#18026);
#14538=AXIS2_PLACEMENT_3D('',#42235,#18027,#18028);
#14539=AXIS2_PLACEMENT_3D('',#42236,#18029,#18030);
#14540=AXIS2_PLACEMENT_3D('',#42237,#18031,#18032);
#14541=AXIS2_PLACEMENT_3D('',#42238,#18033,#18034);
#14542=AXIS2_PLACEMENT_3D('',#42239,#18035,#18036);
#14543=AXIS2_PLACEMENT_3D('',#42240,#18037,#18038);
#14544=AXIS2_PLACEMENT_3D('',#42241,#18039,#18040);
#14545=AXIS2_PLACEMENT_3D('',#42242,#18041,#18042);
#14546=AXIS2_PLACEMENT_3D('',#42243,#18043,#18044);
#14547=AXIS2_PLACEMENT_3D('',#42244,#18045,#18046);
#14548=AXIS2_PLACEMENT_3D('',#42245,#18047,#18048);
#14549=AXIS2_PLACEMENT_3D('',#42246,#18049,#18050);
#14550=AXIS2_PLACEMENT_3D('',#42247,#18051,#18052);
#14551=AXIS2_PLACEMENT_3D('',#42248,#18053,#18054);
#14552=AXIS2_PLACEMENT_3D('',#42249,#18055,#18056);
#14553=AXIS2_PLACEMENT_3D('',#42250,#18057,#18058);
#14554=AXIS2_PLACEMENT_3D('',#42251,#18059,#18060);
#14555=AXIS2_PLACEMENT_3D('',#42252,#18061,#18062);
#14556=AXIS2_PLACEMENT_3D('',#42253,#18063,#18064);
#14557=AXIS2_PLACEMENT_3D('',#42254,#18065,#18066);
#14558=AXIS2_PLACEMENT_3D('',#42255,#18067,#18068);
#14559=AXIS2_PLACEMENT_3D('',#42256,#18069,#18070);
#14560=AXIS2_PLACEMENT_3D('',#42257,#18071,#18072);
#14561=AXIS2_PLACEMENT_3D('',#42258,#18073,#18074);
#14562=AXIS2_PLACEMENT_3D('',#42259,#18075,#18076);
#14563=AXIS2_PLACEMENT_3D('',#42260,#18077,#18078);
#14564=AXIS2_PLACEMENT_3D('',#42261,#18079,#18080);
#14565=AXIS2_PLACEMENT_3D('',#42262,#18081,#18082);
#17443=DIRECTION('axis',(0.,0.,1.));
#17444=DIRECTION('refdir',(1.,0.,0.));
#17445=DIRECTION('center_axis',(0.,-1.83697019872103E-16,-1.));
#17446=DIRECTION('ref_axis',(0.,-1.,1.83697019872103E-16));
#17447=DIRECTION('center_axis',(0.,1.83697019872103E-16,1.));
#17448=DIRECTION('ref_axis',(0.,-1.,1.83697019872103E-16));
#17449=DIRECTION('center_axis',(-1.,1.22464679914735E-16,-2.24963967399279E-32));
#17450=DIRECTION('ref_axis',(1.22464679914735E-16,1.,-1.83697019872103E-16));
#17451=DIRECTION('center_axis',(0.,1.83697019872103E-16,1.));
#17452=DIRECTION('ref_axis',(0.,-1.,1.83697019872103E-16));
#17453=DIRECTION('center_axis',(0.,1.83697019872103E-16,1.));
#17454=DIRECTION('ref_axis',(0.,1.,-2.09599627067876E-16));
#17455=DIRECTION('center_axis',(0.,-1.83697019872103E-16,-1.));
#17456=DIRECTION('ref_axis',(0.,1.,-1.83697019872103E-16));
#17457=DIRECTION('center_axis',(1.,1.22464679914735E-16,-2.24963967399279E-32));
#17458=DIRECTION('ref_axis',(1.22464679914735E-16,-1.,1.30999766917423E-16));
#17459=DIRECTION('center_axis',(0.,1.83697019872103E-16,1.));
#17460=DIRECTION('ref_axis',(0.,1.,-1.83697019872103E-16));
#17461=DIRECTION('center_axis',(0.,1.83697019872103E-16,1.));
#17462=DIRECTION('ref_axis',(0.,1.,-1.83697019872103E-16));
#17463=DIRECTION('center_axis',(0.,-1.83697019872103E-16,-1.));
#17464=DIRECTION('ref_axis',(0.,1.,-1.83697019872103E-16));
#17465=DIRECTION('center_axis',(0.,1.83697019872103E-16,1.));
#17466=DIRECTION('ref_axis',(0.,1.,-2.09599627067876E-16));
#17467=DIRECTION('center_axis',(0.,-1.83697019872103E-16,-1.));
#17468=DIRECTION('ref_axis',(0.,1.,-1.83697019872103E-16));
#17469=DIRECTION('center_axis',(1.,1.22464679914735E-16,-2.24963967399279E-32));
#17470=DIRECTION('ref_axis',(1.22464679914735E-16,-1.,1.30999766917423E-16));
#17471=DIRECTION('center_axis',(0.,1.83697019872103E-16,1.));
#17472=DIRECTION('ref_axis',(0.,-1.,1.83697019872103E-16));
#17473=DIRECTION('center_axis',(0.,-1.83697019872103E-16,-1.));
#17474=DIRECTION('ref_axis',(0.,1.,-1.83697019872103E-16));
#17475=DIRECTION('center_axis',(0.,-1.83697019872103E-16,-1.));
#17476=DIRECTION('ref_axis',(0.,-1.,1.83697019872103E-16));
#17477=DIRECTION('',(8.65956056235483E-17,0.707106781186539,-0.707106781186556));
#17478=DIRECTION('center_axis',(0.,1.83697019872103E-16,1.));
#17479=DIRECTION('ref_axis',(0.,-1.,1.83697019872103E-16));
#17480=DIRECTION('center_axis',(0.,1.83697019872103E-16,1.));
#17481=DIRECTION('ref_axis',(0.,-1.,1.83697019872103E-16));
#17482=DIRECTION('',(0.,1.83697019872103E-16,1.));
#17483=DIRECTION('center_axis',(0.,1.83697019872103E-16,1.));
#17484=DIRECTION('ref_axis',(0.,1.,-1.83697019872103E-16));
#17485=DIRECTION('',(8.65956056235483E-17,-0.707106781186539,0.707106781186556));
#17486=DIRECTION('center_axis',(0.,1.83697019872103E-16,1.));
#17487=DIRECTION('ref_axis',(0.,-1.,1.83697019872103E-16));
#17488=DIRECTION('center_axis',(0.,1.83697019872103E-16,1.));
#17489=DIRECTION('ref_axis',(0.,-1.,1.83697019872103E-16));
#17490=DIRECTION('center_axis',(0.,1.83697019872103E-16,1.));
#17491=DIRECTION('ref_axis',(0.,-1.,1.83697019872103E-16));
#17492=DIRECTION('',(0.,-1.83697019872103E-16,-1.));
#17493=DIRECTION('center_axis',(0.,1.83697019872103E-16,1.));
#17494=DIRECTION('ref_axis',(0.,-1.,1.83697019872103E-16));
#17495=DIRECTION('',(0.,-1.83697019872103E-16,-1.));
#17496=DIRECTION('center_axis',(0.,1.83697019872103E-16,1.));
#17497=DIRECTION('ref_axis',(0.,-1.,1.83697019872103E-16));
#17498=DIRECTION('center_axis',(0.,-1.83697019872103E-16,-1.));
#17499=DIRECTION('ref_axis',(0.,1.,-1.83697019872103E-16));
#17500=DIRECTION('center_axis',(0.,1.83697019872103E-16,1.));
#17501=DIRECTION('ref_axis',(0.,-1.,1.83697019872103E-16));
#17502=DIRECTION('center_axis',(-1.,0.,0.));
#17503=DIRECTION('ref_axis',(0.,1.,0.));
#17504=DIRECTION('center_axis',(0.,1.22464679914735E-16,1.));
#17505=DIRECTION('ref_axis',(0.,-1.,1.22464679914735E-16));
#17506=DIRECTION('center_axis',(-0.623489801858732,0.781831482468031,-1.43620113371566E-16));
#17507=DIRECTION('ref_axis',(0.781831482468031,0.623489801858732,6.91638013500061E-17));
#17508=DIRECTION('center_axis',(-4.78733711238555E-17,1.45519280364738E-16,
1.));
#17509=DIRECTION('ref_axis',(-0.781831482468031,-0.623489801858732,5.33008785647293E-17));
#17510=DIRECTION('center_axis',(0.222520933956319,0.974927912181823,-1.79091352057932E-16));
#17511=DIRECTION('ref_axis',(0.974927912181823,-0.222520933956319,2.24573452299036E-16));
#17512=DIRECTION('center_axis',(-5.96971173526444E-17,1.97322497347747E-16,
1.));
#17513=DIRECTION('ref_axis',(-0.974927912181823,0.222520933956319,-1.02108772384301E-16));
#17514=DIRECTION('center_axis',(0.900968867902422,0.433883739117552,-7.97031498468594E-17));
#17515=DIRECTION('ref_axis',(0.433883739117552,-0.900968867902422,3.4920231590332E-16));
#17516=DIRECTION('center_axis',(-2.65677166156194E-17,2.38865451882509E-16,
1.));
#17517=DIRECTION('ref_axis',(-0.433883739117552,0.900968867902422,-2.26737635988585E-16));
#17518=DIRECTION('center_axis',(0.900968867902416,-0.433883739117565,7.97031498468616E-17));
#17519=DIRECTION('ref_axis',(-0.433883739117565,-0.900968867902416,3.49202315903319E-16));
#17520=DIRECTION('center_axis',(2.65677166156204E-17,2.38865451882508E-16,
1.));
#17521=DIRECTION('ref_axis',(0.433883739117565,0.900968867902416,-2.26737635988584E-16));
#17522=DIRECTION('center_axis',(0.222520933956305,-0.974927912181826,1.79091352057933E-16));
#17523=DIRECTION('ref_axis',(-0.974927912181826,-0.222520933956305,2.24573452299033E-16));
#17524=DIRECTION('center_axis',(5.9697117352644E-17,1.97322497347747E-16,
1.));
#17525=DIRECTION('ref_axis',(0.974927912181826,0.222520933956305,-1.02108772384298E-16));
#17526=DIRECTION('center_axis',(-0.623489801858743,-0.781831482468022,1.43620113371564E-16));
#17527=DIRECTION('ref_axis',(-0.781831482468022,0.623489801858743,6.91638013500039E-17));
#17528=DIRECTION('center_axis',(4.78733711238546E-17,1.45519280364737E-16,
1.));
#17529=DIRECTION('ref_axis',(0.781831482468022,-0.623489801858743,5.33008785647315E-17));
#17530=DIRECTION('center_axis',(0.,1.83697019872103E-16,1.));
#17531=DIRECTION('ref_axis',(0.,1.,-1.62614292875575E-16));
#17532=DIRECTION('center_axis',(0.,-1.83697019872103E-16,-1.));
#17533=DIRECTION('ref_axis',(0.,1.,-1.83697019872103E-16));
#17534=DIRECTION('center_axis',(1.,1.22464679914735E-16,-2.24963967399279E-32));
#17535=DIRECTION('ref_axis',(1.22464679914735E-16,-1.,2.03267866094469E-16));
#17536=DIRECTION('center_axis',(0.,1.83697019872103E-16,1.));
#17537=DIRECTION('ref_axis',(0.,1.,-1.83697019872103E-16));
#17538=DIRECTION('center_axis',(0.,1.83697019872103E-16,1.));
#17539=DIRECTION('ref_axis',(0.,1.,-1.83697019872103E-16));
#17540=DIRECTION('center_axis',(0.,-1.83697019872103E-16,-1.));
#17541=DIRECTION('ref_axis',(0.,-1.,1.64970202400831E-16));
#17542=DIRECTION('center_axis',(0.,1.83697019872103E-16,1.));
#17543=DIRECTION('ref_axis',(0.,-1.,1.83697019872103E-16));
#17544=DIRECTION('center_axis',(1.,-1.22464679914735E-16,2.24963967399279E-32));
#17545=DIRECTION('ref_axis',(1.22464679914735E-16,1.,-2.06212753001039E-16));
#17546=DIRECTION('center_axis',(0.,-1.83697019872103E-16,-1.));
#17547=DIRECTION('ref_axis',(0.,-1.,1.83697019872103E-16));
#17548=DIRECTION('center_axis',(0.,-1.83697019872103E-16,-1.));
#17549=DIRECTION('ref_axis',(0.,-1.,1.62614292875575E-16));
#17550=DIRECTION('center_axis',(0.,1.83697019872103E-16,1.));
#17551=DIRECTION('ref_axis',(0.,-1.,1.83697019872103E-16));
#17552=DIRECTION('center_axis',(1.,-1.22464679914735E-16,2.24963967399279E-32));
#17553=DIRECTION('ref_axis',(1.22464679914735E-16,1.,-2.03267866094469E-16));
#17554=DIRECTION('center_axis',(0.,-1.83697019872103E-16,-1.));
#17555=DIRECTION('ref_axis',(0.,-1.,1.83697019872103E-16));
#17556=DIRECTION('center_axis',(0.,1.83697019872103E-16,1.));
#17557=DIRECTION('ref_axis',(0.,1.,-1.64970202400831E-16));
#17558=DIRECTION('center_axis',(0.,-1.83697019872103E-16,-1.));
#17559=DIRECTION('ref_axis',(0.,1.,-1.83697019872103E-16));
#17560=DIRECTION('center_axis',(1.,1.22464679914735E-16,-2.24963967399279E-32));
#17561=DIRECTION('ref_axis',(1.22464679914735E-16,-1.,2.06212753001039E-16));
#17562=DIRECTION('center_axis',(0.,1.83697019872103E-16,1.));
#17563=DIRECTION('ref_axis',(0.,1.,-1.83697019872103E-16));
#17564=DIRECTION('center_axis',(0.,-1.83697019872103E-16,-1.));
#17565=DIRECTION('ref_axis',(0.,1.,-1.83697019872103E-16));
#17566=DIRECTION('center_axis',(0.,1.83697019872103E-16,1.));
#17567=DIRECTION('ref_axis',(0.,-1.,1.83697019872103E-16));
#17568=DIRECTION('center_axis',(0.,1.83697019872103E-16,1.));
#17569=DIRECTION('ref_axis',(0.,-1.,1.83697019872103E-16));
#17570=DIRECTION('',(0.,1.83697019872103E-16,1.));
#17571=DIRECTION('center_axis',(0.,1.83697019872103E-16,1.));
#17572=DIRECTION('ref_axis',(0.,-1.,1.83697019872103E-16));
#17573=DIRECTION('center_axis',(0.,1.83697019872103E-16,1.));
#17574=DIRECTION('ref_axis',(0.,-1.,1.83697019872103E-16));
#17575=DIRECTION('',(0.,1.83697019872103E-16,1.));
#17576=DIRECTION('center_axis',(0.,1.83697019872103E-16,1.));
#17577=DIRECTION('ref_axis',(0.,-1.,1.83697019872103E-16));
#17578=DIRECTION('center_axis',(0.,1.83697019872103E-16,1.));
#17579=DIRECTION('ref_axis',(0.,-1.,1.83697019872103E-16));
#17580=DIRECTION('center_axis',(0.,1.83697019872103E-16,1.));
#17581=DIRECTION('ref_axis',(0.,-1.,1.83697019872103E-16));
#17582=DIRECTION('',(0.,1.83697019872103E-16,1.));
#17583=DIRECTION('center_axis',(0.,-1.83697019872103E-16,-1.));
#17584=DIRECTION('ref_axis',(0.,-1.,1.83697019872103E-16));
#17585=DIRECTION('center_axis',(-1.,1.22464679914735E-16,-2.24963967399279E-32));
#17586=DIRECTION('ref_axis',(1.22464679914735E-16,1.,-1.83697019872103E-16));
#17587=DIRECTION('center_axis',(0.,1.83697019872103E-16,1.));
#17588=DIRECTION('ref_axis',(0.,-1.,1.83697019872103E-16));
#17589=DIRECTION('center_axis',(0.,1.83697019872103E-16,1.));
#17590=DIRECTION('ref_axis',(0.,-1.,1.83697019872103E-16));
#17591=DIRECTION('',(0.,1.83697019872103E-16,1.));
#17592=DIRECTION('center_axis',(0.,1.83697019872103E-16,1.));
#17593=DIRECTION('ref_axis',(0.,-1.,1.83697019872103E-16));
#17594=DIRECTION('center_axis',(0.,1.83697019872103E-16,1.));
#17595=DIRECTION('ref_axis',(0.,-1.,1.83697019872103E-16));
#17596=DIRECTION('',(0.,1.83697019872103E-16,1.));
#17597=DIRECTION('center_axis',(0.,1.83697019872103E-16,1.));
#17598=DIRECTION('ref_axis',(0.,-1.,1.83697019872103E-16));
#17599=DIRECTION('center_axis',(0.,1.83697019872103E-16,1.));
#17600=DIRECTION('ref_axis',(0.,-1.,1.83697019872103E-16));
#17601=DIRECTION('',(0.,1.83697019872103E-16,1.));
#17602=DIRECTION('center_axis',(0.,1.83697019872103E-16,1.));
#17603=DIRECTION('ref_axis',(0.,-1.,1.83697019872103E-16));
#17604=DIRECTION('center_axis',(0.,-1.83697019872103E-16,-1.));
#17605=DIRECTION('ref_axis',(0.,-1.,1.83697019872103E-16));
#17606=DIRECTION('center_axis',(0.,1.83697019872103E-16,1.));
#17607=DIRECTION('ref_axis',(0.,-1.,1.83697019872103E-16));
#17608=DIRECTION('',(-8.65956056235488E-17,-0.707106781186543,0.707106781186552));
#17609=DIRECTION('center_axis',(0.,1.83697019872103E-16,1.));
#17610=DIRECTION('ref_axis',(0.,-1.,1.83697019872103E-16));
#17611=DIRECTION('center_axis',(0.,1.83697019872103E-16,1.));
#17612=DIRECTION('ref_axis',(0.,1.,-1.83697019872103E-16));
#17613=DIRECTION('center_axis',(0.,1.83697019872103E-16,1.));
#17614=DIRECTION('ref_axis',(0.,-1.,1.83697019872103E-16));
#17615=DIRECTION('center_axis',(0.,1.83697019872103E-16,1.));
#17616=DIRECTION('ref_axis',(0.,-1.,1.83697019872103E-16));
#17617=DIRECTION('',(-8.65956056235488E-17,0.707106781186543,-0.707106781186552));
#17618=DIRECTION('center_axis',(0.,1.83697019872103E-16,1.));
#17619=DIRECTION('ref_axis',(0.,-1.,1.83697019872103E-16));
#17620=DIRECTION('center_axis',(0.,1.83697019872103E-16,1.));
#17621=DIRECTION('ref_axis',(0.,-1.,1.83697019872103E-16));
#17622=DIRECTION('',(0.,-1.83697019872103E-16,-1.));
#17623=DIRECTION('center_axis',(0.,-1.83697019872103E-16,-1.));
#17624=DIRECTION('ref_axis',(0.,1.,-1.83697019872103E-16));
#17625=DIRECTION('center_axis',(0.,1.83697019872103E-16,1.));
#17626=DIRECTION('ref_axis',(0.,-1.,1.83697019872103E-16));
#17627=DIRECTION('center_axis',(0.,-1.83697019872103E-16,-1.));
#17628=DIRECTION('ref_axis',(0.,1.,-1.83697019872103E-16));
#17629=DIRECTION('center_axis',(0.,1.83697019872103E-16,1.));
#17630=DIRECTION('ref_axis',(0.,-1.,1.83697019872103E-16));
#17631=DIRECTION('center_axis',(0.,-1.83697019872103E-16,-1.));
#17632=DIRECTION('ref_axis',(0.,1.,-1.83697019872103E-16));
#17633=DIRECTION('center_axis',(0.,1.83697019872103E-16,1.));
#17634=DIRECTION('ref_axis',(0.,-1.,1.83697019872103E-16));
#17635=DIRECTION('center_axis',(-0.781831482468031,0.623489801858732,6.91638013500059E-17));
#17636=DIRECTION('ref_axis',(0.,0.,-1.));
#17637=DIRECTION('center_axis',(0.781831482468031,-0.623489801858732,-6.91638013500059E-17));
#17638=DIRECTION('ref_axis',(-5.40744373425995E-17,4.31229247995119E-17,
-1.));
#17639=DIRECTION('center_axis',(0.623489801858732,0.781831482468031,0.));
#17640=DIRECTION('ref_axis',(0.,0.,1.));
#17641=DIRECTION('center_axis',(0.781831482468031,-0.623489801858732,-6.91638013500059E-17));
#17642=DIRECTION('ref_axis',(-5.40744373425995E-17,4.31229247995119E-17,
-1.));
#17643=DIRECTION('center_axis',(0.623489801858732,0.781831482468031,-1.22464679914735E-16));
#17644=DIRECTION('ref_axis',(0.,0.,-1.));
#17645=DIRECTION('center_axis',(1.79091352057932E-16,2.24573452299036E-16,
1.));
#17646=DIRECTION('ref_axis',(-5.50003967499518E-33,-1.,2.24573452299036E-16));
#17647=DIRECTION('center_axis',(1.79091352057932E-16,2.24573452299036E-16,
1.));
#17648=DIRECTION('ref_axis',(-5.5000396749952E-33,-1.,2.24573452299036E-16));
#17649=DIRECTION('center_axis',(1.79091352057932E-16,2.24573452299036E-16,
1.));
#17650=DIRECTION('ref_axis',(-5.50003967499518E-33,-1.,2.24573452299036E-16));
#17651=DIRECTION('center_axis',(-0.781831482468031,0.623489801858732,0.));
#17652=DIRECTION('ref_axis',(0.,0.,1.));
#17653=DIRECTION('center_axis',(1.43620113371566E-16,6.91638013500059E-17,
1.));
#17654=DIRECTION('ref_axis',(0.623489801858732,0.781831482468031,-1.43620113371566E-16));
#17655=DIRECTION('center_axis',(1.43620113371566E-16,6.91638013500059E-17,
1.));
#17656=DIRECTION('ref_axis',(0.623489801858732,0.781831482468031,-1.43620113371566E-16));
#17657=DIRECTION('center_axis',(1.43620113371566E-16,6.91638013500059E-17,
1.));
#17658=DIRECTION('ref_axis',(0.623489801858732,0.781831482468031,-1.43620113371566E-16));
#17659=DIRECTION('center_axis',(0.781831482468031,-0.623489801858732,-6.91638013500059E-17));
#17660=DIRECTION('ref_axis',(-5.40744373425995E-17,4.31229247995119E-17,
-1.));
#17661=DIRECTION('center_axis',(0.781831482468031,-0.623489801858732,-6.91638013500059E-17));
#17662=DIRECTION('ref_axis',(-5.40744373425995E-17,4.31229247995119E-17,
-1.));
#17663=DIRECTION('center_axis',(-0.974927912181823,-0.222520933956318,2.24573452299036E-16));
#17664=DIRECTION('ref_axis',(0.,-2.10741377257197E-16,-1.));
#17665=DIRECTION('center_axis',(0.974927912181823,0.222520933956318,-2.24573452299036E-16));
#17666=DIRECTION('ref_axis',(-1.71433215598957E-16,-2.58125940401653E-16,
-1.));
#17667=DIRECTION('center_axis',(-0.222520933956318,0.974927912181823,-3.85233095511903E-16));
#17668=DIRECTION('ref_axis',(0.,3.95140082357245E-16,1.));
#17669=DIRECTION('center_axis',(0.974927912181823,0.222520933956318,-2.24573452299036E-16));
#17670=DIRECTION('ref_axis',(-1.71433215598957E-16,-2.58125940401653E-16,
-1.));
#17671=DIRECTION('center_axis',(-0.222520933956318,0.974927912181823,-3.59586625308286E-16));
#17672=DIRECTION('ref_axis',(0.,-2.4905725751517E-16,-1.));
#17673=DIRECTION('center_axis',(7.97031498468594E-17,3.4920231590332E-16,
1.));
#17674=DIRECTION('ref_axis',(2.39882519785021E-33,-1.,3.4920231590332E-16));
#17675=DIRECTION('center_axis',(7.97031498468594E-17,3.4920231590332E-16,
1.));
#17676=DIRECTION('ref_axis',(2.39882519785021E-33,-1.,3.4920231590332E-16));
#17677=DIRECTION('center_axis',(7.97031498468594E-17,3.4920231590332E-16,
1.));
#17678=DIRECTION('ref_axis',(2.39882519785021E-33,-1.,3.4920231590332E-16));
#17679=DIRECTION('center_axis',(-0.974927912181823,-0.222520933956318,6.92755669385935E-17));
#17680=DIRECTION('ref_axis',(0.,3.11321571893962E-16,1.));
#17681=DIRECTION('center_axis',(1.79091352057932E-16,2.24573452299036E-16,
1.));
#17682=DIRECTION('ref_axis',(-0.222520933956318,0.974927912181823,-1.79091352057933E-16));
#17683=DIRECTION('center_axis',(1.79091352057932E-16,2.24573452299036E-16,
1.));
#17684=DIRECTION('ref_axis',(-0.222520933956318,0.974927912181823,-1.79091352057933E-16));
#17685=DIRECTION('center_axis',(1.79091352057932E-16,2.24573452299036E-16,
1.));
#17686=DIRECTION('ref_axis',(-0.222520933956318,0.974927912181823,-1.79091352057933E-16));
#17687=DIRECTION('center_axis',(0.974927912181823,0.222520933956318,-2.24573452299036E-16));
#17688=DIRECTION('ref_axis',(-1.64444757441796E-16,-2.88744376156862E-16,
-1.));
#17689=DIRECTION('center_axis',(0.974927912181823,0.222520933956318,-2.24573452299036E-16));
#17690=DIRECTION('ref_axis',(-1.64444757441796E-16,-2.88744376156862E-16,
-1.));
#17691=DIRECTION('center_axis',(-0.433883739117553,-0.900968867902422,3.4920231590332E-16));
#17692=DIRECTION('ref_axis',(0.,-4.21482754514395E-16,-1.));
#17693=DIRECTION('center_axis',(0.433883739117553,0.900968867902422,-3.4920231590332E-16));
#17694=DIRECTION('ref_axis',(1.97058769816641E-17,-3.97075180104293E-16,
-1.));
#17695=DIRECTION('center_axis',(-0.900968867902422,0.433883739117553,-2.28593141877839E-16));
#17696=DIRECTION('ref_axis',(0.,5.26853443142994E-16,1.));
#17697=DIRECTION('center_axis',(0.433883739117553,0.900968867902422,-3.4920231590332E-16));
#17698=DIRECTION('ref_axis',(1.97058769816641E-17,-3.97075180104293E-16,
-1.));
#17699=DIRECTION('center_axis',(-0.900968867902422,0.433883739117552,-3.33523066916777E-16));
#17700=DIRECTION('ref_axis',(0.,-4.9811451503034E-16,-1.));
#17701=DIRECTION('center_axis',(-7.97031498468617E-17,3.49202315903319E-16,
1.));
#17702=DIRECTION('ref_axis',(-2.39882519785018E-33,-1.,3.49202315903319E-16));
#17703=DIRECTION('center_axis',(-7.97031498468617E-17,3.49202315903319E-16,
1.));
#17704=DIRECTION('ref_axis',(-2.39882519785018E-33,-1.,3.49202315903319E-16));
#17705=DIRECTION('center_axis',(-7.97031498468617E-17,3.49202315903319E-16,
1.));
#17706=DIRECTION('ref_axis',(-2.39882519785018E-33,-1.,3.49202315903319E-16));
#17707=DIRECTION('center_axis',(-0.433883739117552,-0.900968867902422,5.60982088365811E-16));
#17708=DIRECTION('ref_axis',(0.,6.22643143787925E-16,1.));
#17709=DIRECTION('center_axis',(7.97031498468594E-17,3.4920231590332E-16,
1.));
#17710=DIRECTION('ref_axis',(-0.900968867902422,0.433883739117553,-7.97031498468594E-17));
#17711=DIRECTION('center_axis',(7.97031498468594E-17,3.4920231590332E-16,
1.));
#17712=DIRECTION('ref_axis',(-0.900968867902422,0.433883739117553,-7.97031498468594E-17));
#17713=DIRECTION('center_axis',(7.97031498468594E-17,3.4920231590332E-16,
1.));
#17714=DIRECTION('ref_axis',(-0.900968867902422,0.433883739117553,-7.97031498468594E-17));
#17715=DIRECTION('center_axis',(0.433883739117553,0.900968867902422,-3.4920231590332E-16));
#17716=DIRECTION('ref_axis',(4.4891409918625E-17,-4.09203893527874E-16,
-1.));
#17717=DIRECTION('center_axis',(0.433883739117553,0.900968867902422,-3.4920231590332E-16));
#17718=DIRECTION('ref_axis',(4.48914099186251E-17,-4.09203893527874E-16,
-1.));
#17719=DIRECTION('center_axis',(0.433883739117565,-0.900968867902416,3.49202315903319E-16));
#17720=DIRECTION('ref_axis',(0.,-4.21482754514395E-16,-1.));
#17721=DIRECTION('center_axis',(-0.433883739117565,0.900968867902416,-3.49202315903319E-16));
#17722=DIRECTION('ref_axis',(-1.97058769816642E-17,-3.97075180104295E-16,
-1.));
#17723=DIRECTION('center_axis',(-0.900968867902416,-0.433883739117565,2.28593141877845E-16));
#17724=DIRECTION('ref_axis',(0.,5.26853443142994E-16,1.));
#17725=DIRECTION('center_axis',(-0.433883739117565,0.900968867902416,-3.49202315903319E-16));
#17726=DIRECTION('ref_axis',(-1.97058769816642E-17,-3.97075180104295E-16,
-1.));
#17727=DIRECTION('center_axis',(-0.900968867902416,-0.433883739117565,8.85937070873124E-17));
#17728=DIRECTION('ref_axis',(0.,-4.9811451503034E-16,-1.));
#17729=DIRECTION('center_axis',(-1.79091352057933E-16,2.24573452299033E-16,
1.));
#17730=DIRECTION('ref_axis',(5.50003967499563E-33,-1.,2.24573452299033E-16));
#17731=DIRECTION('center_axis',(-1.79091352057933E-16,2.24573452299033E-16,
1.));
#17732=DIRECTION('ref_axis',(5.50003967499563E-33,-1.,2.24573452299033E-16));
#17733=DIRECTION('center_axis',(-1.79091352057933E-16,2.24573452299033E-16,
1.));
#17734=DIRECTION('ref_axis',(5.50003967499563E-33,-1.,2.24573452299033E-16));
#17735=DIRECTION('center_axis',(0.433883739117565,-0.900968867902416,5.60982088365808E-16));
#17736=DIRECTION('ref_axis',(0.,6.22643143787925E-16,1.));
#17737=DIRECTION('center_axis',(-7.97031498468617E-17,3.49202315903319E-16,
1.));
#17738=DIRECTION('ref_axis',(-0.900968867902416,-0.433883739117565,7.97031498468616E-17));
#17739=DIRECTION('center_axis',(-7.97031498468617E-17,3.49202315903319E-16,
1.));
#17740=DIRECTION('ref_axis',(-0.900968867902416,-0.433883739117565,7.97031498468616E-17));
#17741=DIRECTION('center_axis',(-7.97031498468617E-17,3.49202315903319E-16,
1.));
#17742=DIRECTION('ref_axis',(-0.900968867902416,-0.433883739117565,7.97031498468616E-17));
#17743=DIRECTION('center_axis',(-0.433883739117565,0.900968867902416,-3.49202315903319E-16));
#17744=DIRECTION('ref_axis',(-4.48914099186257E-17,-4.09203893527877E-16,
-1.));
#17745=DIRECTION('center_axis',(-0.433883739117565,0.900968867902416,-3.49202315903319E-16));
#17746=DIRECTION('ref_axis',(-4.48914099186258E-17,-4.09203893527877E-16,
-1.));
#17747=DIRECTION('center_axis',(0.974927912181826,-0.222520933956305,2.24573452299033E-16));
#17748=DIRECTION('ref_axis',(0.,-2.10741377257197E-16,-1.));
#17749=DIRECTION('center_axis',(-0.974927912181826,0.222520933956305,-2.24573452299033E-16));
#17750=DIRECTION('ref_axis',(1.71433215598957E-16,-2.58125940401651E-16,
-1.));
#17751=DIRECTION('center_axis',(-0.222520933956305,-0.974927912181826,1.28411031837301E-16));
#17752=DIRECTION('ref_axis',(0.,1.31713360785748E-16,1.));
#17753=DIRECTION('center_axis',(-0.974927912181826,0.222520933956305,-2.24573452299033E-16));
#17754=DIRECTION('ref_axis',(1.71433215598957E-16,-2.58125940401651E-16,
-1.));
#17755=DIRECTION('center_axis',(-0.222520933956305,-0.974927912181826,1.14657265478815E-16));
#17756=DIRECTION('ref_axis',(0.,-1.24528628757585E-16,-1.));
#17757=DIRECTION('center_axis',(-1.43620113371564E-16,6.91638013500039E-17,
1.));
#17758=DIRECTION('ref_axis',(1.,1.10509814492259E-33,1.43620113371564E-16));
#17759=DIRECTION('center_axis',(-1.43620113371564E-16,6.91638013500039E-17,
1.));
#17760=DIRECTION('ref_axis',(1.,1.10509814492259E-33,1.43620113371564E-16));
#17761=DIRECTION('center_axis',(-1.43620113371564E-16,6.91638013500039E-17,
1.));
#17762=DIRECTION('ref_axis',(1.,1.10509814492259E-33,1.43620113371564E-16));
#17763=DIRECTION('center_axis',(0.974927912181826,-0.222520933956305,3.46377834692947E-17));
#17764=DIRECTION('ref_axis',(0.,1.55660785946981E-16,1.));
#17765=DIRECTION('center_axis',(-1.79091352057933E-16,2.24573452299033E-16,
1.));
#17766=DIRECTION('ref_axis',(-0.222520933956305,-0.974927912181826,1.79091352057932E-16));
#17767=DIRECTION('center_axis',(-1.79091352057933E-16,2.24573452299033E-16,
1.));
#17768=DIRECTION('ref_axis',(-0.222520933956305,-0.974927912181826,1.79091352057932E-16));
#17769=DIRECTION('center_axis',(-1.79091352057933E-16,2.24573452299033E-16,
1.));
#17770=DIRECTION('ref_axis',(-0.222520933956305,-0.974927912181826,1.79091352057932E-16));
#17771=DIRECTION('center_axis',(-0.974927912181826,0.222520933956305,-2.24573452299033E-16));
#17772=DIRECTION('ref_axis',(1.64444757441797E-16,-2.8874437615686E-16,
-1.));
#17773=DIRECTION('center_axis',(-0.974927912181826,0.222520933956305,-2.24573452299033E-16));
#17774=DIRECTION('ref_axis',(1.64444757441797E-16,-2.8874437615686E-16,
-1.));
#17775=DIRECTION('center_axis',(0.781831482468022,0.623489801858743,6.91638013500039E-17));
#17776=DIRECTION('ref_axis',(0.,0.,-1.));
#17777=DIRECTION('center_axis',(-0.781831482468022,-0.623489801858743,-6.91638013500039E-17));
#17778=DIRECTION('ref_axis',(5.40744373425973E-17,4.31229247995114E-17,
-1.));
#17779=DIRECTION('center_axis',(0.623489801858743,-0.781831482468022,-2.05955304247934E-16));
#17780=DIRECTION('ref_axis',(0.,-2.63426721571497E-16,1.));
#17781=DIRECTION('center_axis',(-0.781831482468022,-0.623489801858743,-6.91638013500039E-17));
#17782=DIRECTION('ref_axis',(5.40744373425973E-17,4.31229247995114E-17,
-1.));
#17783=DIRECTION('center_axis',(0.623489801858743,-0.781831482468022,-1.22464679914735E-16));
#17784=DIRECTION('ref_axis',(0.,0.,-1.));
#17785=DIRECTION('center_axis',(0.,0.,-1.));
#17786=DIRECTION('ref_axis',(1.,0.,0.));
#17787=DIRECTION('center_axis',(0.781831482468022,0.623489801858743,0.));
#17788=DIRECTION('ref_axis',(0.,0.,1.));
#17789=DIRECTION('center_axis',(-1.43620113371564E-16,6.91638013500039E-17,
1.));
#17790=DIRECTION('ref_axis',(0.623489801858743,-0.781831482468022,1.43620113371564E-16));
#17791=DIRECTION('center_axis',(-1.43620113371564E-16,6.91638013500039E-17,
1.));
#17792=DIRECTION('ref_axis',(0.623489801858743,-0.781831482468022,1.43620113371564E-16));
#17793=DIRECTION('center_axis',(-1.43620113371564E-16,6.91638013500039E-17,
1.));
#17794=DIRECTION('ref_axis',(0.623489801858743,-0.781831482468022,1.43620113371564E-16));
#17795=DIRECTION('center_axis',(0.,0.,-1.));
#17796=DIRECTION('ref_axis',(1.,0.,0.));
#17797=DIRECTION('center_axis',(0.,0.,-1.));
#17798=DIRECTION('ref_axis',(1.,0.,0.));
#17799=DIRECTION('center_axis',(-0.781831482468022,-0.623489801858743,-6.91638013500039E-17));
#17800=DIRECTION('ref_axis',(5.40744373425973E-17,4.31229247995114E-17,
-1.));
#17801=DIRECTION('center_axis',(-0.781831482468022,-0.623489801858743,-6.91638013500039E-17));
#17802=DIRECTION('ref_axis',(5.40744373425973E-17,4.31229247995114E-17,
-1.));
#17803=DIRECTION('center_axis',(1.,0.,-1.22464679914735E-16));
#17804=DIRECTION('ref_axis',(-6.12323399573677E-17,0.,-1.));
#17805=DIRECTION('center_axis',(1.43620113371566E-16,6.91638013500059E-17,
1.));
#17806=DIRECTION('ref_axis',(1.,-1.10509814492274E-33,-1.43620113371566E-16));
#17807=DIRECTION('center_axis',(1.43620113371566E-16,6.91638013500059E-17,
1.));
#17808=DIRECTION('ref_axis',(1.,-1.10509814492274E-33,-1.43620113371566E-16));
#17809=DIRECTION('center_axis',(1.43620113371566E-16,6.91638013500059E-17,
1.));
#17810=DIRECTION('ref_axis',(1.,-1.10509814492274E-33,-1.43620113371566E-16));
#17811=DIRECTION('center_axis',(0.,1.,0.));
#17812=DIRECTION('ref_axis',(6.12323399573677E-17,0.,1.));
#17813=DIRECTION('center_axis',(0.,0.,1.));
#17814=DIRECTION('ref_axis',(1.,0.,0.));
#17815=DIRECTION('center_axis',(0.,0.,1.));
#17816=DIRECTION('ref_axis',(1.,0.,0.));
#17817=DIRECTION('center_axis',(0.,0.,1.));
#17818=DIRECTION('ref_axis',(1.,0.,0.));
#17819=DIRECTION('center_axis',(0.,-1.,0.));
#17820=DIRECTION('ref_axis',(0.,0.,-1.));
#17821=DIRECTION('center_axis',(0.,-1.,0.));
#17822=DIRECTION('ref_axis',(0.,0.,-1.));
#17823=DIRECTION('center_axis',(0.,1.,0.));
#17824=DIRECTION('ref_axis',(0.,0.,-1.));
#17825=DIRECTION('center_axis',(0.,-1.,0.));
#17826=DIRECTION('ref_axis',(0.,0.,-1.));
#17827=DIRECTION('center_axis',(1.,0.,-1.22464679914735E-16));
#17828=DIRECTION('ref_axis',(1.22464679914735E-16,0.,1.));
#17829=DIRECTION('center_axis',(0.,-1.,0.));
#17830=DIRECTION('ref_axis',(0.,0.,-1.));
#17831=DIRECTION('center_axis',(0.,0.,-1.));
#17832=DIRECTION('ref_axis',(-1.,0.,0.));
#17833=DIRECTION('center_axis',(0.,0.,-1.));
#17834=DIRECTION('ref_axis',(1.,0.,0.));
#17835=DIRECTION('center_axis',(0.,0.,-1.));
#17836=DIRECTION('ref_axis',(1.,0.,0.));
#17837=DIRECTION('center_axis',(0.,0.,-1.));
#17838=DIRECTION('ref_axis',(-1.,0.,0.));
#17839=DIRECTION('center_axis',(0.,0.,1.));
#17840=DIRECTION('ref_axis',(1.,0.,0.));
#17841=DIRECTION('center_axis',(0.,0.,1.));
#17842=DIRECTION('ref_axis',(1.,0.,0.));
#17843=DIRECTION('center_axis',(0.,0.,1.));
#17844=DIRECTION('ref_axis',(1.,0.,0.));
#17845=DIRECTION('center_axis',(0.,0.,1.));
#17846=DIRECTION('ref_axis',(1.,0.,0.));
#17847=DIRECTION('center_axis',(0.,-1.,0.));
#17848=DIRECTION('ref_axis',(0.,0.,-1.));
#17849=DIRECTION('center_axis',(0.,1.,0.));
#17850=DIRECTION('ref_axis',(0.,0.,1.));
#17851=DIRECTION('center_axis',(0.,0.,1.));
#17852=DIRECTION('ref_axis',(1.,0.,0.));
#17853=DIRECTION('center_axis',(0.,0.,-1.));
#17854=DIRECTION('ref_axis',(1.,0.,0.));
#17855=DIRECTION('center_axis',(0.,0.,1.));
#17856=DIRECTION('ref_axis',(1.,0.,0.));
#17857=DIRECTION('center_axis',(0.,0.,1.));
#17858=DIRECTION('ref_axis',(1.,0.,0.));
#17859=DIRECTION('center_axis',(0.,0.,1.));
#17860=DIRECTION('ref_axis',(1.,0.,0.));
#17861=DIRECTION('center_axis',(0.,0.,-1.));
#17862=DIRECTION('ref_axis',(1.,0.,0.));
#17863=DIRECTION('center_axis',(0.,0.,-1.));
#17864=DIRECTION('ref_axis',(-1.,0.,0.));
#17865=DIRECTION('center_axis',(0.,0.,-1.));
#17866=DIRECTION('ref_axis',(-1.,0.,0.));
#17867=DIRECTION('center_axis',(0.781831482468022,0.623489801858743,6.91638013500039E-17));
#17868=DIRECTION('ref_axis',(-1.43620113371564E-16,6.91638013500039E-17,
1.));
#17869=DIRECTION('center_axis',(-0.781831482468022,-0.623489801858743,-6.91638013500039E-17));
#17870=DIRECTION('ref_axis',(1.43620113371564E-16,-6.91638013500039E-17,
-1.));
#17871=DIRECTION('center_axis',(-1.43620113371564E-16,6.91638013500039E-17,
1.));
#17872=DIRECTION('ref_axis',(0.623489801858743,-0.781831482468022,1.43620113371564E-16));
#17873=DIRECTION('center_axis',(-1.43620113371564E-16,6.91638013500039E-17,
1.));
#17874=DIRECTION('ref_axis',(0.623489801858743,-0.781831482468022,1.43620113371564E-16));
#17875=DIRECTION('center_axis',(1.43620113371564E-16,-6.91638013500039E-17,
-1.));
#17876=DIRECTION('ref_axis',(0.623489801858743,-0.781831482468022,1.43620113371564E-16));
#17877=DIRECTION('center_axis',(-1.43620113371564E-16,6.91638013500039E-17,
1.));
#17878=DIRECTION('ref_axis',(0.623489801858743,-0.781831482468022,1.43620113371564E-16));
#17879=DIRECTION('center_axis',(1.43620113371564E-16,-6.91638013500039E-17,
-1.));
#17880=DIRECTION('ref_axis',(0.623489801858743,-0.781831482468022,1.43620113371564E-16));
#17881=DIRECTION('center_axis',(-1.43620113371564E-16,6.91638013500039E-17,
1.));
#17882=DIRECTION('ref_axis',(0.623489801858743,-0.781831482468022,1.43620113371564E-16));
#17883=DIRECTION('center_axis',(1.43620113371564E-16,-6.91638013500039E-17,
-1.));
#17884=DIRECTION('ref_axis',(-0.623489801858743,0.781831482468022,-1.43620113371564E-16));
#17885=DIRECTION('center_axis',(1.43620113371564E-16,-6.91638013500039E-17,
-1.));
#17886=DIRECTION('ref_axis',(-0.623489801858743,0.781831482468022,-1.43620113371564E-16));
#17887=DIRECTION('center_axis',(1.79091352057933E-16,-2.24573452299033E-16,
-1.));
#17888=DIRECTION('ref_axis',(0.222520933956305,0.974927912181826,-1.79091352057932E-16));
#17889=DIRECTION('center_axis',(1.79091352057933E-16,-2.24573452299033E-16,
-1.));
#17890=DIRECTION('ref_axis',(-0.222520933956305,-0.974927912181826,1.79091352057932E-16));
#17891=DIRECTION('center_axis',(1.79091352057933E-16,-2.24573452299033E-16,
-1.));
#17892=DIRECTION('ref_axis',(-0.222520933956305,-0.974927912181826,1.79091352057932E-16));
#17893=DIRECTION('center_axis',(1.79091352057933E-16,-2.24573452299033E-16,
-1.));
#17894=DIRECTION('ref_axis',(0.222520933956305,0.974927912181826,-1.79091352057932E-16));
#17895=DIRECTION('center_axis',(-1.79091352057933E-16,2.24573452299033E-16,
1.));
#17896=DIRECTION('ref_axis',(-0.222520933956305,-0.974927912181826,1.79091352057932E-16));
#17897=DIRECTION('center_axis',(-1.79091352057933E-16,2.24573452299033E-16,
1.));
#17898=DIRECTION('ref_axis',(-0.222520933956305,-0.974927912181826,1.79091352057932E-16));
#17899=DIRECTION('center_axis',(-1.79091352057933E-16,2.24573452299033E-16,
1.));
#17900=DIRECTION('ref_axis',(-0.222520933956305,-0.974927912181826,1.79091352057932E-16));
#17901=DIRECTION('center_axis',(-1.79091352057933E-16,2.24573452299033E-16,
1.));
#17902=DIRECTION('ref_axis',(-0.222520933956305,-0.974927912181826,1.79091352057932E-16));
#17903=DIRECTION('center_axis',(0.974927912181826,-0.222520933956305,2.24573452299033E-16));
#17904=DIRECTION('ref_axis',(-1.79091352057933E-16,2.24573452299033E-16,
1.));
#17905=DIRECTION('center_axis',(-0.974927912181826,0.222520933956305,-2.24573452299033E-16));
#17906=DIRECTION('ref_axis',(1.79091352057933E-16,-2.24573452299033E-16,
-1.));
#17907=DIRECTION('center_axis',(-1.79091352057933E-16,2.24573452299033E-16,
1.));
#17908=DIRECTION('ref_axis',(-0.222520933956305,-0.974927912181826,1.79091352057932E-16));
#17909=DIRECTION('center_axis',(-1.79091352057933E-16,2.24573452299033E-16,
1.));
#17910=DIRECTION('ref_axis',(-0.222520933956305,-0.974927912181826,1.79091352057932E-16));
#17911=DIRECTION('center_axis',(1.79091352057933E-16,-2.24573452299033E-16,
-1.));
#17912=DIRECTION('ref_axis',(-0.222520933956305,-0.974927912181826,1.79091352057932E-16));
#17913=DIRECTION('center_axis',(-1.79091352057933E-16,2.24573452299033E-16,
1.));
#17914=DIRECTION('ref_axis',(-0.222520933956305,-0.974927912181826,1.79091352057932E-16));
#17915=DIRECTION('center_axis',(1.79091352057933E-16,-2.24573452299033E-16,
-1.));
#17916=DIRECTION('ref_axis',(-0.222520933956305,-0.974927912181826,1.79091352057932E-16));
#17917=DIRECTION('center_axis',(-1.79091352057933E-16,2.24573452299033E-16,
1.));
#17918=DIRECTION('ref_axis',(-0.222520933956305,-0.974927912181826,1.79091352057932E-16));
#17919=DIRECTION('center_axis',(1.79091352057933E-16,-2.24573452299033E-16,
-1.));
#17920=DIRECTION('ref_axis',(0.222520933956305,0.974927912181826,-1.79091352057932E-16));
#17921=DIRECTION('center_axis',(1.79091352057933E-16,-2.24573452299033E-16,
-1.));
#17922=DIRECTION('ref_axis',(0.222520933956305,0.974927912181826,-1.79091352057932E-16));
#17923=DIRECTION('center_axis',(7.97031498468617E-17,-3.49202315903319E-16,
-1.));
#17924=DIRECTION('ref_axis',(0.900968867902416,0.433883739117565,-7.97031498468616E-17));
#17925=DIRECTION('center_axis',(7.97031498468617E-17,-3.49202315903319E-16,
-1.));
#17926=DIRECTION('ref_axis',(-0.900968867902416,-0.433883739117565,7.97031498468616E-17));
#17927=DIRECTION('center_axis',(7.97031498468617E-17,-3.49202315903319E-16,
-1.));
#17928=DIRECTION('ref_axis',(-0.900968867902416,-0.433883739117565,7.97031498468616E-17));
#17929=DIRECTION('center_axis',(7.97031498468617E-17,-3.49202315903319E-16,
-1.));
#17930=DIRECTION('ref_axis',(0.900968867902416,0.433883739117565,-7.97031498468616E-17));
#17931=DIRECTION('center_axis',(-7.97031498468617E-17,3.49202315903319E-16,
1.));
#17932=DIRECTION('ref_axis',(-0.900968867902416,-0.433883739117565,7.97031498468616E-17));
#17933=DIRECTION('center_axis',(-7.97031498468617E-17,3.49202315903319E-16,
1.));
#17934=DIRECTION('ref_axis',(-0.900968867902416,-0.433883739117565,7.97031498468616E-17));
#17935=DIRECTION('center_axis',(-7.97031498468617E-17,3.49202315903319E-16,
1.));
#17936=DIRECTION('ref_axis',(-0.900968867902416,-0.433883739117565,7.97031498468616E-17));
#17937=DIRECTION('center_axis',(-7.97031498468617E-17,3.49202315903319E-16,
1.));
#17938=DIRECTION('ref_axis',(-0.900968867902416,-0.433883739117565,7.97031498468616E-17));
#17939=DIRECTION('center_axis',(0.433883739117565,-0.900968867902416,3.49202315903319E-16));
#17940=DIRECTION('ref_axis',(-7.97031498468617E-17,3.49202315903319E-16,
1.));
#17941=DIRECTION('center_axis',(-0.433883739117565,0.900968867902416,-3.49202315903319E-16));
#17942=DIRECTION('ref_axis',(7.97031498468617E-17,-3.49202315903319E-16,
-1.));
#17943=DIRECTION('center_axis',(-7.97031498468617E-17,3.49202315903319E-16,
1.));
#17944=DIRECTION('ref_axis',(-0.900968867902416,-0.433883739117565,7.97031498468616E-17));
#17945=DIRECTION('center_axis',(-7.97031498468617E-17,3.49202315903319E-16,
1.));
#17946=DIRECTION('ref_axis',(-0.900968867902416,-0.433883739117565,7.97031498468616E-17));
#17947=DIRECTION('center_axis',(7.97031498468617E-17,-3.49202315903319E-16,
-1.));
#17948=DIRECTION('ref_axis',(-0.900968867902416,-0.433883739117565,7.97031498468616E-17));
#17949=DIRECTION('center_axis',(-7.97031498468617E-17,3.49202315903319E-16,
1.));
#17950=DIRECTION('ref_axis',(-0.900968867902416,-0.433883739117565,7.97031498468616E-17));
#17951=DIRECTION('center_axis',(7.97031498468617E-17,-3.49202315903319E-16,
-1.));
#17952=DIRECTION('ref_axis',(-0.900968867902416,-0.433883739117565,7.97031498468616E-17));
#17953=DIRECTION('center_axis',(-7.97031498468617E-17,3.49202315903319E-16,
1.));
#17954=DIRECTION('ref_axis',(-0.900968867902416,-0.433883739117565,7.97031498468616E-17));
#17955=DIRECTION('center_axis',(7.97031498468617E-17,-3.49202315903319E-16,
-1.));
#17956=DIRECTION('ref_axis',(0.900968867902416,0.433883739117565,-7.97031498468616E-17));
#17957=DIRECTION('center_axis',(7.97031498468617E-17,-3.49202315903319E-16,
-1.));
#17958=DIRECTION('ref_axis',(0.900968867902416,0.433883739117565,-7.97031498468616E-17));
#17959=DIRECTION('center_axis',(-7.97031498468594E-17,-3.4920231590332E-16,
-1.));
#17960=DIRECTION('ref_axis',(0.900968867902422,-0.433883739117553,7.97031498468594E-17));
#17961=DIRECTION('center_axis',(-7.97031498468594E-17,-3.4920231590332E-16,
-1.));
#17962=DIRECTION('ref_axis',(-0.900968867902422,0.433883739117553,-7.97031498468594E-17));
#17963=DIRECTION('center_axis',(-7.97031498468594E-17,-3.4920231590332E-16,
-1.));
#17964=DIRECTION('ref_axis',(-0.900968867902422,0.433883739117553,-7.97031498468594E-17));
#17965=DIRECTION('center_axis',(-7.97031498468594E-17,-3.4920231590332E-16,
-1.));
#17966=DIRECTION('ref_axis',(0.900968867902422,-0.433883739117553,7.97031498468594E-17));
#17967=DIRECTION('center_axis',(7.97031498468594E-17,3.4920231590332E-16,
1.));
#17968=DIRECTION('ref_axis',(-0.900968867902422,0.433883739117553,-7.97031498468594E-17));
#17969=DIRECTION('center_axis',(7.97031498468594E-17,3.4920231590332E-16,
1.));
#17970=DIRECTION('ref_axis',(-0.900968867902422,0.433883739117553,-7.97031498468594E-17));
#17971=DIRECTION('center_axis',(7.97031498468594E-17,3.4920231590332E-16,
1.));
#17972=DIRECTION('ref_axis',(-0.900968867902422,0.433883739117553,-7.97031498468594E-17));
#17973=DIRECTION('center_axis',(7.97031498468594E-17,3.4920231590332E-16,
1.));
#17974=DIRECTION('ref_axis',(-0.900968867902422,0.433883739117553,-7.97031498468594E-17));
#17975=DIRECTION('center_axis',(-0.433883739117553,-0.900968867902422,3.4920231590332E-16));
#17976=DIRECTION('ref_axis',(7.97031498468594E-17,3.4920231590332E-16,1.));
#17977=DIRECTION('center_axis',(0.433883739117553,0.900968867902422,-3.4920231590332E-16));
#17978=DIRECTION('ref_axis',(-7.97031498468594E-17,-3.4920231590332E-16,
-1.));
#17979=DIRECTION('center_axis',(7.97031498468594E-17,3.4920231590332E-16,
1.));
#17980=DIRECTION('ref_axis',(-0.900968867902422,0.433883739117553,-7.97031498468594E-17));
#17981=DIRECTION('center_axis',(7.97031498468594E-17,3.4920231590332E-16,
1.));
#17982=DIRECTION('ref_axis',(-0.900968867902422,0.433883739117553,-7.97031498468594E-17));
#17983=DIRECTION('center_axis',(-7.97031498468594E-17,-3.4920231590332E-16,
-1.));
#17984=DIRECTION('ref_axis',(-0.900968867902422,0.433883739117553,-7.97031498468594E-17));
#17985=DIRECTION('center_axis',(7.97031498468594E-17,3.4920231590332E-16,
1.));
#17986=DIRECTION('ref_axis',(-0.900968867902422,0.433883739117553,-7.97031498468594E-17));
#17987=DIRECTION('center_axis',(-7.97031498468594E-17,-3.4920231590332E-16,
-1.));
#17988=DIRECTION('ref_axis',(-0.900968867902422,0.433883739117553,-7.97031498468594E-17));
#17989=DIRECTION('center_axis',(7.97031498468594E-17,3.4920231590332E-16,
1.));
#17990=DIRECTION('ref_axis',(-0.900968867902422,0.433883739117553,-7.97031498468594E-17));
#17991=DIRECTION('center_axis',(-7.97031498468594E-17,-3.4920231590332E-16,
-1.));
#17992=DIRECTION('ref_axis',(0.900968867902422,-0.433883739117553,7.97031498468594E-17));
#17993=DIRECTION('center_axis',(-7.97031498468594E-17,-3.4920231590332E-16,
-1.));
#17994=DIRECTION('ref_axis',(0.900968867902422,-0.433883739117553,7.97031498468594E-17));
#17995=DIRECTION('center_axis',(-1.79091352057932E-16,-2.24573452299036E-16,
-1.));
#17996=DIRECTION('ref_axis',(0.222520933956318,-0.974927912181823,1.79091352057933E-16));
#17997=DIRECTION('center_axis',(-1.79091352057932E-16,-2.24573452299036E-16,
-1.));
#17998=DIRECTION('ref_axis',(-0.222520933956318,0.974927912181823,-1.79091352057933E-16));
#17999=DIRECTION('center_axis',(-1.79091352057932E-16,-2.24573452299036E-16,
-1.));
#18000=DIRECTION('ref_axis',(-0.222520933956318,0.974927912181823,-1.79091352057933E-16));
#18001=DIRECTION('center_axis',(-1.79091352057932E-16,-2.24573452299036E-16,
-1.));
#18002=DIRECTION('ref_axis',(0.222520933956318,-0.974927912181823,1.79091352057933E-16));
#18003=DIRECTION('center_axis',(1.79091352057932E-16,2.24573452299036E-16,
1.));
#18004=DIRECTION('ref_axis',(-0.222520933956318,0.974927912181823,-1.79091352057933E-16));
#18005=DIRECTION('center_axis',(1.79091352057932E-16,2.24573452299036E-16,
1.));
#18006=DIRECTION('ref_axis',(-0.222520933956318,0.974927912181823,-1.79091352057933E-16));
#18007=DIRECTION('center_axis',(1.79091352057932E-16,2.24573452299036E-16,
1.));
#18008=DIRECTION('ref_axis',(-0.222520933956318,0.974927912181823,-1.79091352057933E-16));
#18009=DIRECTION('center_axis',(1.79091352057932E-16,2.24573452299036E-16,
1.));
#18010=DIRECTION('ref_axis',(-0.222520933956318,0.974927912181823,-1.79091352057933E-16));
#18011=DIRECTION('center_axis',(-0.974927912181823,-0.222520933956318,2.24573452299036E-16));
#18012=DIRECTION('ref_axis',(1.79091352057932E-16,2.24573452299036E-16,
1.));
#18013=DIRECTION('center_axis',(0.974927912181823,0.222520933956318,-2.24573452299036E-16));
#18014=DIRECTION('ref_axis',(-1.79091352057932E-16,-2.24573452299036E-16,
-1.));
#18015=DIRECTION('center_axis',(1.79091352057932E-16,2.24573452299036E-16,
1.));
#18016=DIRECTION('ref_axis',(-0.222520933956318,0.974927912181823,-1.79091352057933E-16));
#18017=DIRECTION('center_axis',(1.79091352057932E-16,2.24573452299036E-16,
1.));
#18018=DIRECTION('ref_axis',(-0.222520933956318,0.974927912181823,-1.79091352057933E-16));
#18019=DIRECTION('center_axis',(-1.79091352057932E-16,-2.24573452299036E-16,
-1.));
#18020=DIRECTION('ref_axis',(-0.222520933956318,0.974927912181823,-1.79091352057933E-16));
#18021=DIRECTION('center_axis',(1.79091352057932E-16,2.24573452299036E-16,
1.));
#18022=DIRECTION('ref_axis',(-0.222520933956318,0.974927912181823,-1.79091352057933E-16));
#18023=DIRECTION('center_axis',(-1.79091352057932E-16,-2.24573452299036E-16,
-1.));
#18024=DIRECTION('ref_axis',(-0.222520933956318,0.974927912181823,-1.79091352057933E-16));
#18025=DIRECTION('center_axis',(1.79091352057932E-16,2.24573452299036E-16,
1.));
#18026=DIRECTION('ref_axis',(-0.222520933956318,0.974927912181823,-1.79091352057933E-16));
#18027=DIRECTION('center_axis',(-1.79091352057932E-16,-2.24573452299036E-16,
-1.));
#18028=DIRECTION('ref_axis',(0.222520933956318,-0.974927912181823,1.79091352057933E-16));
#18029=DIRECTION('center_axis',(-1.79091352057932E-16,-2.24573452299036E-16,
-1.));
#18030=DIRECTION('ref_axis',(0.222520933956318,-0.974927912181823,1.79091352057933E-16));
#18031=DIRECTION('center_axis',(-1.43620113371566E-16,-6.91638013500059E-17,
-1.));
#18032=DIRECTION('ref_axis',(-0.623489801858732,-0.781831482468031,1.43620113371566E-16));
#18033=DIRECTION('center_axis',(-1.43620113371566E-16,-6.91638013500059E-17,
-1.));
#18034=DIRECTION('ref_axis',(0.623489801858732,0.781831482468031,-1.43620113371566E-16));
#18035=DIRECTION('center_axis',(-1.43620113371566E-16,-6.91638013500059E-17,
-1.));
#18036=DIRECTION('ref_axis',(0.623489801858732,0.781831482468031,-1.43620113371566E-16));
#18037=DIRECTION('center_axis',(-1.43620113371566E-16,-6.91638013500059E-17,
-1.));
#18038=DIRECTION('ref_axis',(-0.623489801858732,-0.781831482468031,1.43620113371566E-16));
#18039=DIRECTION('center_axis',(1.43620113371566E-16,6.91638013500059E-17,
1.));
#18040=DIRECTION('ref_axis',(0.623489801858732,0.781831482468031,-1.43620113371566E-16));
#18041=DIRECTION('center_axis',(1.43620113371566E-16,6.91638013500059E-17,
1.));
#18042=DIRECTION('ref_axis',(0.623489801858732,0.781831482468031,-1.43620113371566E-16));
#18043=DIRECTION('center_axis',(1.43620113371566E-16,6.91638013500059E-17,
1.));
#18044=DIRECTION('ref_axis',(0.623489801858732,0.781831482468031,-1.43620113371566E-16));
#18045=DIRECTION('center_axis',(1.43620113371566E-16,6.91638013500059E-17,
1.));
#18046=DIRECTION('ref_axis',(0.623489801858732,0.781831482468031,-1.43620113371566E-16));
#18047=DIRECTION('center_axis',(-0.781831482468031,0.623489801858732,6.91638013500059E-17));
#18048=DIRECTION('ref_axis',(1.43620113371566E-16,6.91638013500061E-17,
1.));
#18049=DIRECTION('center_axis',(0.781831482468031,-0.623489801858732,-6.91638013500059E-17));
#18050=DIRECTION('ref_axis',(-1.43620113371566E-16,-6.91638013500061E-17,
-1.));
#18051=DIRECTION('center_axis',(1.43620113371566E-16,6.91638013500059E-17,
1.));
#18052=DIRECTION('ref_axis',(0.623489801858732,0.781831482468031,-1.43620113371566E-16));
#18053=DIRECTION('center_axis',(1.43620113371566E-16,6.91638013500059E-17,
1.));
#18054=DIRECTION('ref_axis',(0.623489801858732,0.781831482468031,-1.43620113371566E-16));
#18055=DIRECTION('center_axis',(-1.43620113371566E-16,-6.91638013500059E-17,
-1.));
#18056=DIRECTION('ref_axis',(0.623489801858732,0.781831482468031,-1.43620113371566E-16));
#18057=DIRECTION('center_axis',(1.43620113371566E-16,6.91638013500059E-17,
1.));
#18058=DIRECTION('ref_axis',(0.623489801858732,0.781831482468031,-1.43620113371566E-16));
#18059=DIRECTION('center_axis',(-1.43620113371566E-16,-6.91638013500059E-17,
-1.));
#18060=DIRECTION('ref_axis',(0.623489801858732,0.781831482468031,-1.43620113371566E-16));
#18061=DIRECTION('center_axis',(1.43620113371566E-16,6.91638013500059E-17,
1.));
#18062=DIRECTION('ref_axis',(0.623489801858732,0.781831482468031,-1.43620113371566E-16));
#18063=DIRECTION('center_axis',(-1.43620113371566E-16,-6.91638013500059E-17,
-1.));
#18064=DIRECTION('ref_axis',(-0.623489801858732,-0.781831482468031,1.43620113371566E-16));
#18065=DIRECTION('center_axis',(-1.43620113371566E-16,-6.91638013500059E-17,
-1.));
#18066=DIRECTION('ref_axis',(-0.623489801858732,-0.781831482468031,1.43620113371566E-16));
#18067=DIRECTION('center_axis',(0.,0.,1.));
#18068=DIRECTION('ref_axis',(1.,0.,0.));
#18069=DIRECTION('center_axis',(0.,0.,1.));
#18070=DIRECTION('ref_axis',(1.,0.,0.));
#18071=DIRECTION('center_axis',(0.,0.,-1.));
#18072=DIRECTION('ref_axis',(1.,0.,0.));
#18073=DIRECTION('center_axis',(0.,0.,1.));
#18074=DIRECTION('ref_axis',(1.,0.,0.));
#18075=DIRECTION('center_axis',(0.,0.,-1.));
#18076=DIRECTION('ref_axis',(1.,0.,0.));
#18077=DIRECTION('center_axis',(0.,0.,1.));
#18078=DIRECTION('ref_axis',(1.,0.,0.));
#18079=DIRECTION('center_axis',(0.,0.,-1.));
#18080=DIRECTION('ref_axis',(-1.,0.,0.));
#18081=DIRECTION('center_axis',(0.,0.,-1.));
#18082=DIRECTION('ref_axis',(-1.,0.,0.));
#40850=CARTESIAN_POINT('',(0.,0.,0.));
#40851=CARTESIAN_POINT('Origin',(0.,1.73472347597681E-15,6.67403582113016E-15));
#40852=CARTESIAN_POINT('',(1.52656933693714E-15,12.4653846153846,-3.0875));
#40853=CARTESIAN_POINT('Origin',(0.,6.26866080313552E-16,-3.0875));
#40854=CARTESIAN_POINT('',(-1.52656933693714E-15,12.4653846153846,3.0875));
#40855=CARTESIAN_POINT('Origin',(1.74512168878498E-15,14.25,4.05635328795269E-15));
#40856=CARTESIAN_POINT('Origin',(0.,1.76119517802379E-15,3.0875));
#40857=CARTESIAN_POINT('Origin',(0.,1.56496838953657E-16,-5.64807088834312));
#40858=CARTESIAN_POINT('',(9.67029207191279E-16,7.64278544417155,-5.99278544417156));
#40859=CARTESIAN_POINT('',(9.35971273077467E-16,-7.64278544417155,-5.99278544417156));
#40860=CARTESIAN_POINT('Origin',(0.,9.31738023414375E-17,-5.99278544417156));
#40861=CARTESIAN_POINT('',(9.18485099360515E-16,-7.5,-5.64807088834312));
#40862=CARTESIAN_POINT('Origin',(9.78186630818948E-16,-7.9875,-5.64807088834312));
#40863=CARTESIAN_POINT('',(9.18485099360515E-16,7.5,-5.64807088834312));
#40864=CARTESIAN_POINT('Origin',(0.,1.56496838953657E-16,-5.64807088834312));
#40865=CARTESIAN_POINT('Origin',(0.,1.56496838953657E-16,-5.64807088834312));
#40866=CARTESIAN_POINT('Origin',(0.,9.31738023414375E-17,-5.99278544417156));
#40867=CARTESIAN_POINT('Origin',(0.,2.23156441938368E-15,5.64807088834312));
#40868=CARTESIAN_POINT('',(9.18485099360515E-16,7.5,5.64807088834312));
#40869=CARTESIAN_POINT('',(9.18485099360515E-16,-7.5,5.64807088834312));
#40870=CARTESIAN_POINT('Origin',(0.,2.23156441938368E-15,5.64807088834312));
#40871=CARTESIAN_POINT('',(-9.35971273077467E-16,-7.64278544417155,5.99278544417156));
#40872=CARTESIAN_POINT('Origin',(9.78186630818948E-16,-7.9875,5.64807088834312));
#40873=CARTESIAN_POINT('Origin',(0.,2.2948874559959E-15,5.99278544417156));
#40874=CARTESIAN_POINT('Origin',(0.,2.23156441938368E-15,5.64807088834312));
#40875=CARTESIAN_POINT('Origin',(0.,-9.99635681210842E-31,-6.5));
#40876=CARTESIAN_POINT('',(-9.98087141305092E-16,8.14999999999999,-6.50000000000001));
#40877=CARTESIAN_POINT('',(9.98087141305092E-16,8.14999999999999,-6.5));
#40878=CARTESIAN_POINT('Origin',(0.,-9.99635681210842E-31,-6.5));
#40879=CARTESIAN_POINT('Origin',(0.,0.,-6.5));
#40880=CARTESIAN_POINT('',(-9.18485099360515E-16,7.5,-6.5));
#40881=CARTESIAN_POINT('Origin',(0.,2.26865819542047E-15,5.85));
#40882=CARTESIAN_POINT('',(-9.98087141305091E-16,-8.14999999999998,6.50000000000001));
#40883=CARTESIAN_POINT('',(9.18485099360515E-16,-7.5,5.85));
#40884=CARTESIAN_POINT('Origin',(0.,2.38806125833734E-15,6.50000000000001));
#40885=CARTESIAN_POINT('Origin',(0.,0.,-6.5));
#40886=CARTESIAN_POINT('',(-1.52656933693714E-15,12.4653846153846,6.50000000000001));
#40887=CARTESIAN_POINT('Origin',(0.,2.38806125833734E-15,6.50000000000001));
#40888=CARTESIAN_POINT('',(-1.52656933693714E-15,12.4653846153846,-6.5));
#40889=CARTESIAN_POINT('Origin',(0.,0.,-6.5));
#40890=CARTESIAN_POINT('',(-1.52656933693714E-15,12.4653846153846,-6.50000000000001));
#40891=CARTESIAN_POINT('',(-1.52656933693714E-15,12.4653846153846,-6.5));
#40892=CARTESIAN_POINT('Origin',(0.,-1.17267830746035E-30,-6.50000000000001));
#40893=CARTESIAN_POINT('Origin',(0.,8.14999999999999,-6.50000000000001));
#40894=CARTESIAN_POINT('Origin',(0.,8.14999999999999,6.50000000000001));
#40895=CARTESIAN_POINT('Origin',(0.,14.25,4.07195060716495E-15));
#40896=CARTESIAN_POINT('',(-3.56616156686793,14.25,4.07195060716495E-15));
#40897=CARTESIAN_POINT('',(3.56616156686793,14.25,4.07195060716495E-15));
#40898=CARTESIAN_POINT('Origin',(0.,14.25,4.07195060716495E-15));
#40899=CARTESIAN_POINT('Origin',(11.1410986251694,8.88472967648693,5.05753477640253E-15));
#40900=CARTESIAN_POINT('',(8.91763325644669,11.6728670610318,4.54536224786764E-15));
#40901=CARTESIAN_POINT('',(13.3645639938921,6.09659229194206,5.56970730493742E-15));
#40902=CARTESIAN_POINT('Origin',(11.1410986251694,8.88472967648693,5.05753477640253E-15));
#40903=CARTESIAN_POINT('Origin',(13.892722748591,-3.17092330887753,7.27212230242621E-15));
#40904=CARTESIAN_POINT('',(14.6862683510896,0.305827142012077,6.6334536057588E-15));
#40905=CARTESIAN_POINT('',(13.0991771460924,-6.64767375976714,7.91079099909362E-15));
#40906=CARTESIAN_POINT('Origin',(13.892722748591,-3.17092330887753,7.27212230242621E-15));
#40907=CARTESIAN_POINT('Origin',(6.18284328242512,-12.8388063676095,9.04808360878726E-15));
#40908=CARTESIAN_POINT('',(9.39584383208325,-11.2915068526795,8.76384929904507E-15));
#40909=CARTESIAN_POINT('',(2.96984273276699,-14.3861058825395,9.33231791852945E-15));
#40910=CARTESIAN_POINT('Origin',(6.18284328242512,-12.8388063676095,9.04808360878726E-15));
#40911=CARTESIAN_POINT('Origin',(-6.1828432824253,-12.8388063676094,9.04808360878725E-15));
#40912=CARTESIAN_POINT('',(-2.9698427327672,-14.3861058825394,9.33231791852944E-15));
#40913=CARTESIAN_POINT('',(-9.39584383208341,-11.2915068526794,8.76384929904506E-15));
#40914=CARTESIAN_POINT('Origin',(-6.1828432824253,-12.8388063676094,9.04808360878725E-15));
#40915=CARTESIAN_POINT('Origin',(-13.892722748591,-3.17092330887735,7.27212230242617E-15));
#40916=CARTESIAN_POINT('',(-13.0991771460925,-6.64767375976697,7.91079099909359E-15));
#40917=CARTESIAN_POINT('',(-14.6862683510895,0.30582714201227,6.63345360575876E-15));
#40918=CARTESIAN_POINT('Origin',(-13.892722748591,-3.17092330887735,7.27212230242617E-15));
#40919=CARTESIAN_POINT('Origin',(-11.1410986251693,8.88472967648709,5.0575347764025E-15));
#40920=CARTESIAN_POINT('',(-13.3645639938921,6.09659229194225,5.56970730493739E-15));
#40921=CARTESIAN_POINT('',(-8.91763325644655,11.6728670610319,4.54536224786761E-15));
#40922=CARTESIAN_POINT('Origin',(-11.1410986251693,8.88472967648709,5.0575347764025E-15));
#40923=CARTESIAN_POINT('Origin',(0.,1.07462756625201E-17,-6.44149999999999));
#40924=CARTESIAN_POINT('',(-1.99949495950787E-15,-16.3271153846154,-6.49999999999999));
#40925=CARTESIAN_POINT('Origin',(0.,2.01169401222323E-30,-6.49999999999999));
#40926=CARTESIAN_POINT('',(1.99233077573286E-15,-16.2686153846154,-6.44149999999999));
#40927=CARTESIAN_POINT('Origin',(1.99949495950788E-15,-16.3271153846154,
-6.44149999999999));
#40928=CARTESIAN_POINT('',(1.99233077573286E-15,16.2686153846154,-6.44149999999999));
#40929=CARTESIAN_POINT('Origin',(0.,1.07462756625199E-17,-6.44149999999999));
#40930=CARTESIAN_POINT('Origin',(0.,1.07462756625199E-17,-6.44149999999999));
#40931=CARTESIAN_POINT('Origin',(0.,1.30149338579385E-16,-5.7915));
#40932=CARTESIAN_POINT('',(-1.96367404063281E-15,16.0346153846154,-5.7915));
#40933=CARTESIAN_POINT('Origin',(0.,1.30149338579385E-16,-5.7915));
#40934=CARTESIAN_POINT('',(-1.97083822440782E-15,16.0931153846154,-5.85));
#40935=CARTESIAN_POINT('Origin',(1.97083822440783E-15,16.0931153846154,
-5.7915));
#40936=CARTESIAN_POINT('Origin',(0.,1.19403062916867E-16,-5.85));
#40937=CARTESIAN_POINT('Origin',(0.,2.37731498267482E-15,6.44150000000001));
#40938=CARTESIAN_POINT('',(-1.99949495950787E-15,16.3271153846154,6.5));
#40939=CARTESIAN_POINT('Origin',(0.,2.38806125833734E-15,6.50000000000001));
#40940=CARTESIAN_POINT('',(-1.99233077573286E-15,16.2686153846154,6.4415));
#40941=CARTESIAN_POINT('Origin',(1.99949495950788E-15,16.3271153846154,
6.44150000000001));
#40942=CARTESIAN_POINT('Origin',(0.,2.37731498267482E-15,6.44150000000001));
#40943=CARTESIAN_POINT('Origin',(0.,2.25791191975795E-15,5.7915));
#40944=CARTESIAN_POINT('',(1.96367404063281E-15,16.0346153846154,5.7915));
#40945=CARTESIAN_POINT('',(1.96367404063282E-15,-16.0346153846154,5.7915));
#40946=CARTESIAN_POINT('Origin',(0.,2.25791191975795E-15,5.7915));
#40947=CARTESIAN_POINT('',(-1.97083822440782E-15,-16.0931153846154,5.85000000000001));
#40948=CARTESIAN_POINT('Origin',(1.97083822440783E-15,-16.0931153846154,
5.7915));
#40949=CARTESIAN_POINT('Origin',(0.,2.26865819542047E-15,5.85));
#40950=CARTESIAN_POINT('Origin',(0.,2.25791191975795E-15,5.7915));
#40951=CARTESIAN_POINT('Origin',(0.,0.,-6.5));
#40952=CARTESIAN_POINT('',(-2.16636878649169E-15,17.6897435897436,-6.084));
#40953=CARTESIAN_POINT('Origin',(0.,7.6417960266795E-17,-6.084));
#40954=CARTESIAN_POINT('',(-2.16636878649169E-15,17.6897435897436,-5.85));
#40955=CARTESIAN_POINT('',(-2.16636878649169E-15,17.6897435897436,-6.5));
#40956=CARTESIAN_POINT('Origin',(0.,1.19403062916867E-16,-5.85));
#40957=CARTESIAN_POINT('Origin',(0.,0.,-6.5));
#40958=CARTESIAN_POINT('',(-1.99233077573286E-15,16.2686153846154,-6.084));
#40959=CARTESIAN_POINT('',(-1.99233077573286E-15,16.2686153846154,-6.5));
#40960=CARTESIAN_POINT('Origin',(0.,7.6417960266795E-17,-6.084));
#40961=CARTESIAN_POINT('Origin',(0.,0.,-6.5));
#40962=CARTESIAN_POINT('',(-1.96367404063281E-15,16.0346153846154,3.0875));
#40963=CARTESIAN_POINT('Origin',(0.,1.76119517802379E-15,3.08750000000001));
#40964=CARTESIAN_POINT('',(-1.96367404063282E-15,16.0346153846154,-6.5));
#40965=CARTESIAN_POINT('Origin',(0.,1.73472347597681E-15,6.67403582113016E-15));
#40966=CARTESIAN_POINT('',(-1.96367404063281E-15,16.0346153846154,-3.0875));
#40967=CARTESIAN_POINT('Origin',(1.74512168878498E-15,14.25,4.05635328795269E-15));
#40968=CARTESIAN_POINT('Origin',(0.,6.26866080313552E-16,-3.08749999999999));
#40969=CARTESIAN_POINT('Origin',(0.,0.,-6.5));
#40970=CARTESIAN_POINT('',(-1.96367404063282E-15,16.0346153846154,-6.5));
#40971=CARTESIAN_POINT('Origin',(0.,0.,-6.5));
#40972=CARTESIAN_POINT('',(-1.99233077573286E-15,16.2686153846154,6.084));
#40973=CARTESIAN_POINT('Origin',(0.,2.31164329807054E-15,6.084));
#40974=CARTESIAN_POINT('',(-1.99233077573286E-15,16.2686153846154,-6.5));
#40975=CARTESIAN_POINT('Origin',(0.,0.,-6.5));
#40976=CARTESIAN_POINT('',(-2.16636878649169E-15,17.6897435897436,5.85));
#40977=CARTESIAN_POINT('Origin',(0.,2.26865819542047E-15,5.85));
#40978=CARTESIAN_POINT('',(-2.16636878649169E-15,17.6897435897436,6.084));
#40979=CARTESIAN_POINT('',(-2.16636878649169E-15,17.6897435897436,-6.5));
#40980=CARTESIAN_POINT('Origin',(0.,2.31164329807054E-15,6.084));
#40981=CARTESIAN_POINT('Origin',(0.,2.38806125833734E-15,6.50000000000001));
#40982=CARTESIAN_POINT('',(-2.57175827820944E-15,21.,5.85));
#40983=CARTESIAN_POINT('Origin',(0.,2.26865819542047E-15,5.85000000000001));
#40984=CARTESIAN_POINT('',(-2.49215623626487E-15,20.35,6.5));
#40985=CARTESIAN_POINT('',(2.49215623626486E-15,20.35,6.50000000000001));
#40986=CARTESIAN_POINT('Origin',(0.,2.38806125833734E-15,6.50000000000001));
#40987=CARTESIAN_POINT('Origin',(0.,1.19403062916869E-16,-5.84999999999999));
#40988=CARTESIAN_POINT('',(2.57175827820944E-15,21.,-5.84999999999999));
#40989=CARTESIAN_POINT('',(2.57175827820944E-15,-21.,-5.84999999999999));
#40990=CARTESIAN_POINT('Origin',(0.,1.19403062916869E-16,-5.84999999999999));
#40991=CARTESIAN_POINT('Origin',(0.,1.19403062916869E-16,-5.84999999999999));
#40992=CARTESIAN_POINT('',(-2.49215623626487E-15,-20.35,-6.49999999999999));
#40993=CARTESIAN_POINT('',(2.57175827820944E-15,-21.,-5.84999999999999));
#40994=CARTESIAN_POINT('Origin',(0.,1.96135664184276E-30,-6.49999999999999));
#40995=CARTESIAN_POINT('Origin',(0.,0.,-6.5));
#40996=CARTESIAN_POINT('',(-2.57175827820944E-15,21.,-6.5));
#40997=CARTESIAN_POINT('Origin',(0.,20.35,-6.49999999999999));
#40998=CARTESIAN_POINT('Origin',(0.,20.35,6.5));
#40999=CARTESIAN_POINT('Origin',(0.,16.0346153846154,5.85));
#41000=CARTESIAN_POINT('Origin',(0.,16.2686153846154,6.084));
#41001=CARTESIAN_POINT('Origin',(0.,16.2686153846154,-6.084));
#41002=CARTESIAN_POINT('Origin',(0.,16.0346153846154,-5.85));
#41003=CARTESIAN_POINT('Origin',(-11.1410986251694,8.88472967648693,9.85584169237584E-16));
#41004=CARTESIAN_POINT('',(-11.838732871064,9.44107442276088,3.96060240207311));
#41005=CARTESIAN_POINT('Origin',(-11.838732871064,9.44107442276088,1.04729956121144E-15));
#41006=CARTESIAN_POINT('',(-10.4434643792749,8.32838493021299,3.96060240207311));
#41007=CARTESIAN_POINT('Origin',(-11.1410986251694,8.88472967648693,2.5198520116158));
#41008=CARTESIAN_POINT('Origin',(-10.4434643792749,8.32838493021299,9.23868777263733E-16));
#41009=CARTESIAN_POINT('',(-13.176267261227,5.42664547033602,-1.08333333333333));
#41010=CARTESIAN_POINT('',(-13.9269936544441,5.94376395877182,-1.08333333333333));
#41011=CARTESIAN_POINT('Ctrl Pts',(-13.176267261227,5.42664547033603,-1.08333333333333));
#41012=CARTESIAN_POINT('Ctrl Pts',(-13.3544742809805,5.48608062863209,-1.08333333333333));
#41013=CARTESIAN_POINT('Ctrl Pts',(-13.5395781511317,5.58798093945111,-1.08333333333333));
#41014=CARTESIAN_POINT('Ctrl Pts',(-13.7657237213497,5.76832601371359,-1.08333333333333));
#41015=CARTESIAN_POINT('Ctrl Pts',(-13.851789663848,5.85187873682469,-1.08333333333333));
#41016=CARTESIAN_POINT('Ctrl Pts',(-13.9269936544446,5.9437639587714,-1.08333333333333));
#41017=CARTESIAN_POINT('',(-13.9269936544455,5.94376395877242,1.08333333333333));
#41018=CARTESIAN_POINT('Ctrl Pts',(-13.9269936544444,5.94376395877114,1.08333333333355));
#41019=CARTESIAN_POINT('Ctrl Pts',(-13.9416885168396,5.90933203032471,0.95688863210348));
#41020=CARTESIAN_POINT('Ctrl Pts',(-13.9536527109306,5.88095561854246,0.828820583351296));
#41021=CARTESIAN_POINT('Ctrl Pts',(-13.9629765258054,5.85873440158612,0.699646919261824));
#41022=CARTESIAN_POINT('Ctrl Pts',(-13.9722513158078,5.83663002439321,0.571152453813156));
#41023=CARTESIAN_POINT('Ctrl Pts',(-13.9789135007646,5.82061622745832,0.441563969171476));
#41024=CARTESIAN_POINT('Ctrl Pts',(-13.9830050237945,5.81077040959789,0.311391073637591));
#41025=CARTESIAN_POINT('Ctrl Pts',(-13.9870637119681,5.80100360534983,0.182262827807202));
#41026=CARTESIAN_POINT('Ctrl Pts',(-13.9885928700523,5.79730615639837,0.0525595133518154));
#41027=CARTESIAN_POINT('Ctrl Pts',(-13.9875862925321,5.79973378332902,-0.0772214321948836));
#41028=CARTESIAN_POINT('Ctrl Pts',(-13.9868997670034,5.80138952054624,-0.16573715053464));
#41029=CARTESIAN_POINT('Ctrl Pts',(-13.9850326975558,5.80589410253377,-0.25428898113034));
#41030=CARTESIAN_POINT('Ctrl Pts',(-13.9819702480149,5.81325986277477,-0.342719102199523));
#41031=CARTESIAN_POINT('Ctrl Pts',(-13.9773533484511,5.82436436418404,-0.476034927301742));
#41032=CARTESIAN_POINT('Ctrl Pts',(-13.9700489046451,5.84190742581559,-0.608312350205735));
#41033=CARTESIAN_POINT('Ctrl Pts',(-13.9600480872369,5.86570879353503,-0.739057191237609));
#41034=CARTESIAN_POINT('Ctrl Pts',(-13.9511688384278,5.8868408927778,-0.855139299994326));
#41035=CARTESIAN_POINT('Ctrl Pts',(-13.9401632237806,5.9129059856334,-0.970013302477931));
#41036=CARTESIAN_POINT('Ctrl Pts',(-13.9269936544444,5.94376395877114,-1.08333333333355));
#41037=CARTESIAN_POINT('',(-13.176267261227,5.42664547033602,1.08333333333333));
#41038=CARTESIAN_POINT('Ctrl Pts',(-13.176267261227,5.42664547033603,1.08333333333333));
#41039=CARTESIAN_POINT('Ctrl Pts',(-13.3544742809805,5.48608062863209,1.08333333333333));
#41040=CARTESIAN_POINT('Ctrl Pts',(-13.5395781511317,5.58798093945111,1.08333333333333));
#41041=CARTESIAN_POINT('Ctrl Pts',(-13.76572372135,5.76832601371385,1.08333333333333));
#41042=CARTESIAN_POINT('Ctrl Pts',(-13.8517896638487,5.85187873682532,1.08333333333333));
#41043=CARTESIAN_POINT('Ctrl Pts',(-13.9269936544455,5.94376395877245,1.08333333333333));
#41044=CARTESIAN_POINT('Ctrl Pts',(-13.176267261227,5.426645470336,-1.08333333333333));
#41045=CARTESIAN_POINT('Ctrl Pts',(-13.1893705593041,5.39482976422217,-0.949270311030458));
#41046=CARTESIAN_POINT('Ctrl Pts',(-13.1999097963793,5.36892368585873,-0.813521288367943));
#41047=CARTESIAN_POINT('Ctrl Pts',(-13.2079621630869,5.34904061477063,-0.676607052100963));
#41048=CARTESIAN_POINT('Ctrl Pts',(-13.2148460430323,5.33204279546006,-0.559560573777783));
#41049=CARTESIAN_POINT('Ctrl Pts',(-13.2199117356377,5.31944645364942,-0.441662516279014));
#41050=CARTESIAN_POINT('Ctrl Pts',(-13.2231796369648,5.31131059989529,-0.323238258334693));
#41051=CARTESIAN_POINT('Ctrl Pts',(-13.2269557156994,5.30190957419894,-0.186398348762648));
#41052=CARTESIAN_POINT('Ctrl Pts',(-13.2283213471704,5.29849241313602,-0.0492519096262365));
#41053=CARTESIAN_POINT('Ctrl Pts',(-13.2273014856384,5.30103720115478,0.0876758270660023));
#41054=CARTESIAN_POINT('Ctrl Pts',(-13.2262786675027,5.30358936657696,0.225000520654269));
#41055=CARTESIAN_POINT('Ctrl Pts',(-13.2228564747501,5.31213809759637,0.362105241912721));
#41056=CARTESIAN_POINT('Ctrl Pts',(-13.21701132539,5.32664168351063,0.498460177595569));
#41057=CARTESIAN_POINT('Ctrl Pts',(-13.2111409592134,5.34120783998416,0.635403368116636));
#41058=CARTESIAN_POINT('Ctrl Pts',(-13.2028266475275,5.36178038996277,0.771590289741212));
#41059=CARTESIAN_POINT('Ctrl Pts',(-13.1919958930595,5.38829698119001,0.90648424252654));
#41060=CARTESIAN_POINT('Ctrl Pts',(-13.1872415508606,5.39993688577963,0.965698216399817));
#41061=CARTESIAN_POINT('Ctrl Pts',(-13.1820016856382,5.4127218947045,1.02466304565395));
#41062=CARTESIAN_POINT('Ctrl Pts',(-13.176267261227,5.426645470336,1.08333333333333));
#41063=CARTESIAN_POINT('',(-8.89378902201695,12.2552029391753,-1.08333333333333));
#41064=CARTESIAN_POINT('',(-8.22258343557141,11.6383685130291,-1.08333333333333));
#41065=CARTESIAN_POINT('Ctrl Pts',(-8.89378902201693,12.2552029391753,-1.08333333333333));
#41066=CARTESIAN_POINT('Ctrl Pts',(-8.78747309219938,12.2023308550396,-1.08333333333333));
#41067=CARTESIAN_POINT('Ctrl Pts',(-8.68686373639314,12.1370149953911,-1.08333333333333));
#41068=CARTESIAN_POINT('Ctrl Pts',(-8.46071816617524,11.9566699211287,-1.08333333333333));
#41069=CARTESIAN_POINT('Ctrl Pts',(-8.32018322283281,11.7988819437994,-1.08333333333333));
#41070=CARTESIAN_POINT('Ctrl Pts',(-8.22258343557192,11.6383685130288,-1.08333333333333));
#41071=CARTESIAN_POINT('',(-8.22258343557665,11.6383685130365,1.08333333333333));
#41072=CARTESIAN_POINT('Ctrl Pts',(-8.22258343557191,11.6383685130287,1.08333333333318));
#41073=CARTESIAN_POINT('Ctrl Pts',(-8.19455490688727,11.6581708517696,0.949622058007629));
#41074=CARTESIAN_POINT('Ctrl Pts',(-8.17172113698899,11.6741565633286,0.814376693553349));
#41075=CARTESIAN_POINT('Ctrl Pts',(-8.15417398891324,11.6864000683928,0.678132403728345));
#41076=CARTESIAN_POINT('Ctrl Pts',(-8.13671023659264,11.698585384152,0.542535637671064));
#41077=CARTESIAN_POINT('Ctrl Pts',(-8.12448291951145,11.7070640382822,0.405949418799179));
#41078=CARTESIAN_POINT('Ctrl Pts',(-8.11755242812626,11.7118675955896,0.268901316712111));
#41079=CARTESIAN_POINT('Ctrl Pts',(-8.11302715126356,11.7150040870061,0.179415511018989));
#41080=CARTESIAN_POINT('Ctrl Pts',(-8.11075954642953,11.7165728598427,0.0897327832367744));
#41081=CARTESIAN_POINT('Ctrl Pts',(-8.11075954642953,11.7165728598427,9.99200722162641E-15));
#41082=CARTESIAN_POINT('Ctrl Pts',(-8.11075954642954,11.7165728598427,-0.137573936980354));
#41083=CARTESIAN_POINT('Ctrl Pts',(-8.11609005089583,11.7128881555246,-0.274951212619692));
#41084=CARTESIAN_POINT('Ctrl Pts',(-8.12669452775723,11.7055258768037,-0.4116124062147));
#41085=CARTESIAN_POINT('Ctrl Pts',(-8.13738105388554,11.6981066344457,-0.549330978772881));
#41086=CARTESIAN_POINT('Ctrl Pts',(-8.15342350530942,11.6869526399855,-0.686322345437031));
#41087=CARTESIAN_POINT('Ctrl Pts',(-8.17473347641523,11.6720277839618,-0.822054935347404));
#41088=CARTESIAN_POINT('Ctrl Pts',(-8.18849695174643,11.662388264195,-0.909720570537357));
#41089=CARTESIAN_POINT('Ctrl Pts',(-8.20445714658991,11.6511748546878,-0.996861109122827));
#41090=CARTESIAN_POINT('Ctrl Pts',(-8.22258343557191,11.6383685130287,-1.08333333333318));
#41091=CARTESIAN_POINT('',(-8.89378902201695,12.2552029391753,1.08333333333333));
#41092=CARTESIAN_POINT('Ctrl Pts',(-8.89378902201693,12.2552029391753,1.08333333333333));
#41093=CARTESIAN_POINT('Ctrl Pts',(-8.78747309219938,12.2023308550396,1.08333333333333));
#41094=CARTESIAN_POINT('Ctrl Pts',(-8.68686373639314,12.1370149953911,1.08333333333333));
#41095=CARTESIAN_POINT('Ctrl Pts',(-8.46071816617751,11.9566699211305,1.08333333333333));
#41096=CARTESIAN_POINT('Ctrl Pts',(-8.32018322283717,11.7988819438045,1.08333333333333));
#41097=CARTESIAN_POINT('Ctrl Pts',(-8.22258343557662,11.6383685130365,1.08333333333333));
#41098=CARTESIAN_POINT('Ctrl Pts',(-8.89378902201696,12.2552029391753,-1.08333333333333));
#41099=CARTESIAN_POINT('Ctrl Pts',(-8.86325700199161,12.2773604951023,-0.955915065626613));
#41100=CARTESIAN_POINT('Ctrl Pts',(-8.83806624000395,12.2954729083691,-0.8267015714506));
#41101=CARTESIAN_POINT('Ctrl Pts',(-8.81837639229442,12.3095783864577,-0.696211209492237));
#41102=CARTESIAN_POINT('Ctrl Pts',(-8.79899689851553,12.3234615321731,-0.567777653525536));
#41103=CARTESIAN_POINT('Ctrl Pts',(-8.7849462329058,12.3334631509294,-0.438107164856251));
#41104=CARTESIAN_POINT('Ctrl Pts',(-8.77634666705863,12.3395794672318,-0.307693975181527));
#41105=CARTESIAN_POINT('Ctrl Pts',(-8.76960830208466,12.3443720314467,-0.205506064179221));
#41106=CARTESIAN_POINT('Ctrl Pts',(-8.76621624622179,12.3467783236356,-0.102862147741002));
#41107=CARTESIAN_POINT('Ctrl Pts',(-8.76621624622179,12.3467783236356,2.44249065417534E-15));
#41108=CARTESIAN_POINT('Ctrl Pts',(-8.76621624622179,12.3467783236356,0.130666807305558));
#41109=CARTESIAN_POINT('Ctrl Pts',(-8.77169236507929,12.3428956683044,0.261069786498707));
#41110=CARTESIAN_POINT('Ctrl Pts',(-8.78256611126601,12.3351536167882,0.390710450871087));
#41111=CARTESIAN_POINT('Ctrl Pts',(-8.79357042167237,12.3273186042172,0.521907748246256));
#41112=CARTESIAN_POINT('Ctrl Pts',(-8.8101027782242,12.315530900308,0.652324314224256));
#41113=CARTESIAN_POINT('Ctrl Pts',(-8.83205039902736,12.2997710546807,0.781443489202971));
#41114=CARTESIAN_POINT('Ctrl Pts',(-8.84930597782606,12.2873804060307,0.882959098491573));
#41115=CARTESIAN_POINT('Ctrl Pts',(-8.86990830867396,12.2725335396739,0.983672743459536));
#41116=CARTESIAN_POINT('Ctrl Pts',(-8.89378902201696,12.2552029391753,1.08333333333333));
#41117=CARTESIAN_POINT('Origin',(-11.1410986251694,8.88472967648693,9.85584169237584E-16));
#41118=CARTESIAN_POINT('',(-13.6377879061429,6.58029051604744,1.08333333333333));
#41119=CARTESIAN_POINT('',(-13.2594869773434,6.22835470309403,1.08333333333333));
#41120=CARTESIAN_POINT('Origin',(-11.1410986251694,8.88472967648693,1.08333333333333));
#41121=CARTESIAN_POINT('',(-13.6377879061429,6.58029051604744,-1.08333333333333));
#41122=CARTESIAN_POINT('Ctrl Pts',(-13.6377879061429,6.58029051604746,-1.08333333333332));
#41123=CARTESIAN_POINT('Ctrl Pts',(-13.6907677796516,6.47048863474076,-0.727666221822785));
#41124=CARTESIAN_POINT('Ctrl Pts',(-13.7154355939007,6.41687686636447,-0.35278297384277));
#41125=CARTESIAN_POINT('Ctrl Pts',(-13.7154355939007,6.41687686636447,0.352782973842772));
#41126=CARTESIAN_POINT('Ctrl Pts',(-13.6907677796516,6.47048863474076,0.727666221822785));
#41127=CARTESIAN_POINT('Ctrl Pts',(-13.6377879061429,6.58029051604746,1.08333333333332));
#41128=CARTESIAN_POINT('',(-12.9276994994136,5.99475484510091,-1.08333333333333));
#41129=CARTESIAN_POINT('Origin',(-11.1410986251694,8.88472967648693,-1.08333333333333));
#41130=CARTESIAN_POINT('',(-12.9276994994136,5.99475484510091,1.08333333333333));
#41131=CARTESIAN_POINT('Ctrl Pts',(-12.9276994994136,5.99475484510092,1.08333333333333));
#41132=CARTESIAN_POINT('Ctrl Pts',(-12.9759843593574,5.89062845864246,0.725928647976576));
#41133=CARTESIAN_POINT('Ctrl Pts',(-12.9982133898606,5.84028669430256,0.352039859176989));
#41134=CARTESIAN_POINT('Ctrl Pts',(-12.9982133898606,5.84028669430256,-0.352039859176986));
#41135=CARTESIAN_POINT('Ctrl Pts',(-12.9759843593574,5.89062845864246,-0.725928647976575));
#41136=CARTESIAN_POINT('Ctrl Pts',(-12.9276994994136,5.99475484510092,-1.08333333333332));
#41137=CARTESIAN_POINT('Origin',(-11.1410986251694,8.88472967648693,1.08333333333333));
#41138=CARTESIAN_POINT('',(-9.02271027299537,11.5411046498798,1.08333333333333));
#41139=CARTESIAN_POINT('Origin',(-11.1410986251694,8.88472967648693,9.85584169237584E-16));
#41140=CARTESIAN_POINT('',(-8.72113759169224,11.2696166353063,1.08333333333333));
#41141=CARTESIAN_POINT('Origin',(-11.1410986251694,8.88472967648693,1.08333333333333));
#41142=CARTESIAN_POINT('',(-8.72113759169224,11.2696166353063,-1.08333333333333));
#41143=CARTESIAN_POINT('Ctrl Pts',(-8.72113759169222,11.2696166353063,-1.08333333333334));
#41144=CARTESIAN_POINT('Ctrl Pts',(-8.63036626326988,11.3398611937656,-0.725928647976585));
#41145=CARTESIAN_POINT('Ctrl Pts',(-8.58623309669495,11.3727349924818,-0.352039859176991));
#41146=CARTESIAN_POINT('Ctrl Pts',(-8.58623309669495,11.3727349924818,4.46574186955748E-16));
#41147=CARTESIAN_POINT('Ctrl Pts',(-8.58623309669495,11.3727349924818,0.352039859176991));
#41148=CARTESIAN_POINT('Ctrl Pts',(-8.63036626326988,11.3398611937656,0.725928647976585));
#41149=CARTESIAN_POINT('Ctrl Pts',(-8.72113759169222,11.2696166353063,1.08333333333334));
#41150=CARTESIAN_POINT('',(-9.45000219633307,11.8316076987796,-1.08333333333333));
#41151=CARTESIAN_POINT('Origin',(-11.1410986251694,8.88472967648693,-1.08333333333333));
#41152=CARTESIAN_POINT('',(-9.45000219633307,11.8316076987796,1.08333333333333));
#41153=CARTESIAN_POINT('Ctrl Pts',(-9.45000219633306,11.8316076987796,1.08333333333334));
#41154=CARTESIAN_POINT('Ctrl Pts',(-9.35474240837113,11.9076924734257,0.727666221822798));
#41155=CARTESIAN_POINT('Ctrl Pts',(-9.30796390402501,11.9436715548398,0.352782973842778));
#41156=CARTESIAN_POINT('Ctrl Pts',(-9.30796390402501,11.9436715548398,5.10741104345864E-16));
#41157=CARTESIAN_POINT('Ctrl Pts',(-9.30796390402501,11.9436715548398,-0.352782973842777));
#41158=CARTESIAN_POINT('Ctrl Pts',(-9.35474240837113,11.9076924734257,-0.727666221822798));
#41159=CARTESIAN_POINT('Ctrl Pts',(-9.45000219633306,11.8316076987796,-1.08333333333334));
#41160=CARTESIAN_POINT('Origin',(-11.1410986251694,8.88472967648693,1.08333333333333));
#41161=CARTESIAN_POINT('',(-10.4434643792749,8.32838493021299,-3.45272288248773));
#41162=CARTESIAN_POINT('Origin',(-10.4434643792749,8.32838493021299,9.23868777263733E-16));
#41163=CARTESIAN_POINT('',(-11.838732871064,9.44107442276088,-3.45272288248773));
#41164=CARTESIAN_POINT('Origin',(-11.838732871064,9.44107442276088,1.04729956121144E-15));
#41165=CARTESIAN_POINT('Origin',(-13.892722748591,-3.17092330887753,3.20017169526126E-15));
#41166=CARTESIAN_POINT('',(-14.7626584240763,-3.36948044994625,3.96060240207311));
#41167=CARTESIAN_POINT('Origin',(-14.7626584240763,-3.36948044994625,3.40056031423578E-15));
#41168=CARTESIAN_POINT('',(-13.0227870731057,-2.97236616780882,3.96060240207311));
#41169=CARTESIAN_POINT('Origin',(-13.892722748591,-3.17092330887753,2.5198520116158));
#41170=CARTESIAN_POINT('Origin',(-13.0227870731057,-2.97236616780882,2.99978307628674E-15));
#41171=CARTESIAN_POINT('',(-12.4579905368413,-6.91816245718267,-1.08333333333333));
#41172=CARTESIAN_POINT('',(-13.3303603014234,-7.18268588222789,-1.08333333333333));
#41173=CARTESIAN_POINT('Ctrl Pts',(-12.4579905368413,-6.91816245718265,
-1.08333333333333));
#41174=CARTESIAN_POINT('Ctrl Pts',(-12.6155690741986,-7.02043310055334,
-1.08333333333333));
#41175=CARTESIAN_POINT('Ctrl Pts',(-12.8106483205941,-7.10161932916232,
-1.08333333333333));
#41176=CARTESIAN_POINT('Ctrl Pts',(-13.0926472341269,-7.16598374096129,
-1.08333333333333));
#41177=CARTESIAN_POINT('Ctrl Pts',(-13.211632620936,-7.18117853359748,-1.08333333333333));
#41178=CARTESIAN_POINT('Ctrl Pts',(-13.3303603014234,-7.18268588222786,
-1.08333333333333));
#41179=CARTESIAN_POINT('',(-13.3303603014234,-7.18268588222787,1.08333333333334));
#41180=CARTESIAN_POINT('Ctrl Pts',(-13.3303603014234,-7.18268588222788,
1.08333333333333));
#41181=CARTESIAN_POINT('Ctrl Pts',(-13.312602432605,-7.21564274452362,0.9568886321034));
#41182=CARTESIAN_POINT('Ctrl Pts',(-13.2978764135175,-7.24268913148589,
0.828820583351364));
#41183=CARTESIAN_POINT('Ctrl Pts',(-13.2863164700111,-7.26383348564883,
0.699646919262042));
#41184=CARTESIAN_POINT('Ctrl Pts',(-13.2748173090022,-7.28486666222222,
0.571152453813466));
#41185=CARTESIAN_POINT('Ctrl Pts',(-13.2664510227833,-7.30005980724142,
0.441563969171881));
#41186=CARTESIAN_POINT('Ctrl Pts',(-13.2613042752926,-7.30939745578436,
0.311391073638092));
#41187=CARTESIAN_POINT('Ctrl Pts',(-13.2561988309335,-7.3186601688214,0.182262827807686));
#41188=CARTESIAN_POINT('Ctrl Pts',(-13.2542614634094,-7.32216103446744,
0.0525595133522827));
#41189=CARTESIAN_POINT('Ctrl Pts',(-13.2555318677528,-7.31986045983868,
-0.0772214321944347));
#41190=CARTESIAN_POINT('Ctrl Pts',(-13.2563983335701,-7.31829137729732,
-0.165737150534351));
#41191=CARTESIAN_POINT('Ctrl Pts',(-13.2587560588234,-7.31402308269238,
-0.254288981130211));
#41192=CARTESIAN_POINT('Ctrl Pts',(-13.2626054360146,-7.30703628683457,
-0.342719102199554));
#41193=CARTESIAN_POINT('Ctrl Pts',(-13.2684086950193,-7.29650310602083,
-0.476034927301584));
#41194=CARTESIAN_POINT('Ctrl Pts',(-13.2775701666804,-7.27985434187078,
-0.608312350205395));
#41195=CARTESIAN_POINT('Ctrl Pts',(-13.2899434176249,-7.25719547792734,
-0.739057191237093));
#41196=CARTESIAN_POINT('Ctrl Pts',(-13.3009290370229,-7.23707775329796,
-0.855139299993907));
#41197=CARTESIAN_POINT('Ctrl Pts',(-13.3144456587151,-7.21222189770289,
-0.970013302477609));
#41198=CARTESIAN_POINT('Ctrl Pts',(-13.3303603014234,-7.18268588222788,
-1.08333333333332));
#41199=CARTESIAN_POINT('',(-12.4579905368413,-6.91816245718267,1.08333333333334));
#41200=CARTESIAN_POINT('Ctrl Pts',(-12.4579905368413,-6.91816245718265,
1.08333333333333));
#41201=CARTESIAN_POINT('Ctrl Pts',(-12.6150882655077,-7.02012104908378,
1.08333333333333));
#41202=CARTESIAN_POINT('Ctrl Pts',(-12.8106174809568,-7.10161229021636,
1.08333333333333));
#41203=CARTESIAN_POINT('Ctrl Pts',(-13.0925863122299,-7.16596983593587,
1.08333333333333));
#41204=CARTESIAN_POINT('Ctrl Pts',(-13.2116839714656,-7.18117918553602,
1.08333333333333));
#41205=CARTESIAN_POINT('Ctrl Pts',(-13.3303603014234,-7.18268588222786,
1.08333333333333));
#41206=CARTESIAN_POINT('Ctrl Pts',(-12.4579905368413,-6.91816245718269,
-1.08333333333333));
#41207=CARTESIAN_POINT('Ctrl Pts',(-12.4412857888864,-6.94824379644449,
-0.949270311030495));
#41208=CARTESIAN_POINT('Ctrl Pts',(-12.4276027080703,-6.97263587945683,
-0.813521288368019));
#41209=CARTESIAN_POINT('Ctrl Pts',(-12.4170780656485,-6.99132836531023,
-0.676607052101084));
#41210=CARTESIAN_POINT('Ctrl Pts',(-12.4080806643214,-7.0073083663671,-0.559560573777871));
#41211=CARTESIAN_POINT('Ctrl Pts',(-12.4013908554087,-7.01912257498617,
-0.441662516279072));
#41212=CARTESIAN_POINT('Ctrl Pts',(-12.3970674919579,-7.02675014497037,
-0.323238258334728));
#41213=CARTESIAN_POINT('Ctrl Pts',(-12.392071820683,-7.03556384585404,-0.186398348762656));
#41214=CARTESIAN_POINT('Ctrl Pts',(-12.3902516338786,-7.03876210460556,
-0.0492519096262199));
#41215=CARTESIAN_POINT('Ctrl Pts',(-12.3916053560034,-7.03637809537454,
0.0876758270660418));
#41216=CARTESIAN_POINT('Ctrl Pts',(-12.3929630026022,-7.03398717484178,
0.22500052065431));
#41217=CARTESIAN_POINT('Ctrl Pts',(-12.3975129673671,-7.02598155019929,
0.36210524191276));
#41218=CARTESIAN_POINT('Ctrl Pts',(-12.4052079364271,-7.0123687905019,0.498460177595606));
#41219=CARTESIAN_POINT('Ctrl Pts',(-12.4129361026924,-6.99869730339788,
0.635403368116707));
#41220=CARTESIAN_POINT('Ctrl Pts',(-12.4238364813948,-6.97937013765694,
0.771590289741313));
#41221=CARTESIAN_POINT('Ctrl Pts',(-12.4378151222667,-6.9543694886247,0.906484242526672));
#41222=CARTESIAN_POINT('Ctrl Pts',(-12.4439512822522,-6.94339503240897,
0.965698216399908));
#41223=CARTESIAN_POINT('Ctrl Pts',(-12.450680002204,-6.93132701813286,1.024663045654));
#41224=CARTESIAN_POINT('Ctrl Pts',(-12.4579905368413,-6.91816245718269,
1.08333333333334));
#41225=CARTESIAN_POINT('',(-15.1266902369927,0.68754979644356,-1.08333333333333));
#41226=CARTESIAN_POINT('',(-14.2259398250621,0.827729480997533,-1.08333333333333));
#41227=CARTESIAN_POINT('Ctrl Pts',(-15.1266902369927,0.687549796443589,
-1.08333333333333));
#41228=CARTESIAN_POINT('Ctrl Pts',(-15.0191128271494,0.737684039417719,
-1.08333333333333));
#41229=CARTESIAN_POINT('Ctrl Pts',(-14.905210454464,0.775655426636244,-1.08333333333333));
#41230=CARTESIAN_POINT('Ctrl Pts',(-14.6232416231909,0.840012972355744,
-1.08333333333333));
#41231=CARTESIAN_POINT('Ctrl Pts',(-14.411718162898,0.851428848194329,-1.08333333333333));
#41232=CARTESIAN_POINT('Ctrl Pts',(-14.2259398250622,0.827729480996923,
-1.08333333333333));
#41233=CARTESIAN_POINT('',(-14.2259398250711,0.827729480998061,1.08333333333334));
#41234=CARTESIAN_POINT('Ctrl Pts',(-14.2259398250621,0.827729480996948,
1.08333333333319));
#41235=CARTESIAN_POINT('Ctrl Pts',(-14.2239464151202,0.86198962338768,0.949622058007746));
#41236=CARTESIAN_POINT('Ctrl Pts',(-14.2222079250172,0.889808711690097,
0.814376693553578));
#41237=CARTESIAN_POINT('Ctrl Pts',(-14.2208398148552,0.911161325029729,
0.678132403728685));
#41238=CARTESIAN_POINT('Ctrl Pts',(-14.2194782068654,0.932412456504284,
0.542535637671376));
#41239=CARTESIAN_POINT('Ctrl Pts',(-14.2184834780892,0.947258512328182,
0.405949418799462));
#41240=CARTESIAN_POINT('Ctrl Pts',(-14.2179179597194,0.955671957675903,
0.268901316712362));
#41241=CARTESIAN_POINT('Ctrl Pts',(-14.2175487034788,0.961165532005871,
0.179415511019154));
#41242=CARTESIAN_POINT('Ctrl Pts',(-14.2173613909827,0.963916530719958,
0.0897327832368514));
#41243=CARTESIAN_POINT('Ctrl Pts',(-14.2173613909827,0.963916530719958,
-1.77635683940025E-15));
#41244=CARTESIAN_POINT('Ctrl Pts',(-14.2173613909827,0.963916530719959,
-0.137573936980362));
#41245=CARTESIAN_POINT('Ctrl Pts',(-14.2178040883167,0.957451598945575,
-0.274951212619699));
#41246=CARTESIAN_POINT('Ctrl Pts',(-14.2186598102071,0.944570379379332,
-0.411612406214706));
#41247=CARTESIAN_POINT('Ctrl Pts',(-14.2195221530139,0.931589494866292,
-0.549330978772852));
#41248=CARTESIAN_POINT('Ctrl Pts',(-14.2208039138492,0.912092599491199,
-0.686322345436968));
#41249=CARTESIAN_POINT('Ctrl Pts',(-14.222421741201,0.886126297665223,-0.82205493534731));
#41250=CARTESIAN_POINT('Ctrl Pts',(-14.2234666476786,0.869355437073727,
-0.909720570537294));
#41251=CARTESIAN_POINT('Ctrl Pts',(-14.2246506698206,0.849885807806941,
-0.996861109122796));
#41252=CARTESIAN_POINT('Ctrl Pts',(-14.2259398250621,0.827729480996951,
-1.08333333333318));
#41253=CARTESIAN_POINT('',(-15.1266902369927,0.687549796443561,1.08333333333334));
#41254=CARTESIAN_POINT('Ctrl Pts',(-15.1266902369927,0.687549796443589,
1.08333333333333));
#41255=CARTESIAN_POINT('Ctrl Pts',(-15.0191128271494,0.73768403941772,1.08333333333333));
#41256=CARTESIAN_POINT('Ctrl Pts',(-14.905210454464,0.775655426636245,1.08333333333333));
#41257=CARTESIAN_POINT('Ctrl Pts',(-14.6232416231937,0.840012972355103,
1.08333333333333));
#41258=CARTESIAN_POINT('Ctrl Pts',(-14.4117181629048,0.851428848194163,
1.08333333333333));
#41259=CARTESIAN_POINT('Ctrl Pts',(-14.2259398250711,0.827729480998062,
1.08333333333333));
#41260=CARTESIAN_POINT('Ctrl Pts',(-15.1266902369927,0.687549796443564,
-1.08333333333333));
#41261=CARTESIAN_POINT('Ctrl Pts',(-15.1249773086751,0.725235701077295,
-0.955915065626697));
#41262=CARTESIAN_POINT('Ctrl Pts',(-15.1234319803901,0.756223536825465,
-0.826701571450772));
#41263=CARTESIAN_POINT('Ctrl Pts',(-15.122183667988,0.780412301388329,-0.696211209492499));
#41264=CARTESIAN_POINT('Ctrl Pts',(-15.1209550316477,0.804219799510246,
-0.567777653525797));
#41265=CARTESIAN_POINT('Ctrl Pts',(-15.12001416535,0.821440959530219,-0.438107164856512));
#41266=CARTESIAN_POINT('Ctrl Pts',(-15.1194343523859,0.83197783168462,-0.307693975181787));
#41267=CARTESIAN_POINT('Ctrl Pts',(-15.1189800281283,0.840234212474348,
-0.205506064179395));
#41268=CARTESIAN_POINT('Ctrl Pts',(-15.1187464308798,0.844386527178334,
-0.102862147741089));
#41269=CARTESIAN_POINT('Ctrl Pts',(-15.1187464308798,0.844386527178334,
1.99840144432528E-15));
#41270=CARTESIAN_POINT('Ctrl Pts',(-15.1187464308798,0.844386527178334,
0.130666807305563));
#41271=CARTESIAN_POINT('Ctrl Pts',(-15.1191251529677,0.837684329050672,
0.261069786498716));
#41272=CARTESIAN_POINT('Ctrl Pts',(-15.1198518432089,0.824355801783686,
0.3907104508711));
#41273=CARTESIAN_POINT('Ctrl Pts',(-15.1205872590302,0.810867235029684,
0.521907748246278));
#41274=CARTESIAN_POINT('Ctrl Pts',(-15.1216790167187,0.790592205023353,
0.652324314224286));
#41275=CARTESIAN_POINT('Ctrl Pts',(-15.1230415909943,0.763606761086714,
0.78144348920301));
#41276=CARTESIAN_POINT('Ctrl Pts',(-15.1241128691977,0.742390363261972,
0.882959098491598));
#41277=CARTESIAN_POINT('Ctrl Pts',(-15.1253504648421,0.717025942629857,
0.983672743459549));
#41278=CARTESIAN_POINT('Ctrl Pts',(-15.1266902369927,0.687549796443564,
1.08333333333333));
#41279=CARTESIAN_POINT('Origin',(-13.892722748591,-3.17092330887753,3.20017169526126E-15));
#41280=CARTESIAN_POINT('',(-13.6476999686241,-6.55970790622096,1.08333333333334));
#41281=CARTESIAN_POINT('',(-13.1366786991091,-6.483368720524,1.08333333333334));
#41282=CARTESIAN_POINT('Origin',(-13.892722748591,-3.17092330887753,1.08333333333334));
#41283=CARTESIAN_POINT('',(-13.6476999686241,-6.55970790622096,-1.08333333333333));
#41284=CARTESIAN_POINT('Ctrl Pts',(-13.6476999686241,-6.55970790622096,
-1.08333333333332));
#41285=CARTESIAN_POINT('Ctrl Pts',(-13.5948858118208,-6.66958959248691,
-0.727666221822786));
#41286=CARTESIAN_POINT('Ctrl Pts',(-13.5683505740919,-6.72230205711272,
-0.35278297384277));
#41287=CARTESIAN_POINT('Ctrl Pts',(-13.5683505740919,-6.72230205711272,
0.352782973842779));
#41288=CARTESIAN_POINT('Ctrl Pts',(-13.5948858118208,-6.66958959248691,
0.727666221822796));
#41289=CARTESIAN_POINT('Ctrl Pts',(-13.6476999686241,-6.55970790622096,
1.08333333333333));
#41290=CARTESIAN_POINT('',(-12.7471768669563,-6.36961395396413,-1.08333333333333));
#41291=CARTESIAN_POINT('Origin',(-13.892722748591,-3.17092330887754,-1.08333333333333));
#41292=CARTESIAN_POINT('',(-12.7471768669563,-6.36961395396413,1.08333333333334));
#41293=CARTESIAN_POINT('Ctrl Pts',(-12.7471768669563,-6.36961395396412,
1.08333333333334));
#41294=CARTESIAN_POINT('Ctrl Pts',(-12.6958726976266,-6.472286317656,0.725928647976585));
#41295=CARTESIAN_POINT('Ctrl Pts',(-12.6703734952066,-6.52105325020167,
0.352039859176994));
#41296=CARTESIAN_POINT('Ctrl Pts',(-12.6703734952066,-6.52105325020167,
-0.352039859176985));
#41297=CARTESIAN_POINT('Ctrl Pts',(-12.6958726976266,-6.472286317656,-0.725928647976576));
#41298=CARTESIAN_POINT('Ctrl Pts',(-12.7471768669563,-6.36961395396413,
-1.08333333333333));
#41299=CARTESIAN_POINT('Origin',(-13.892722748591,-3.17092330887753,1.08333333333334));
#41300=CARTESIAN_POINT('',(-14.6487667980729,0.141522102768936,1.08333333333334));
#41301=CARTESIAN_POINT('Origin',(-13.892722748591,-3.17092330887753,3.20017169526126E-15));
#41302=CARTESIAN_POINT('',(-14.2484814298548,0.208031110850571,1.08333333333334));
#41303=CARTESIAN_POINT('Origin',(-13.892722748591,-3.17092330887753,1.08333333333334));
#41304=CARTESIAN_POINT('',(-14.2484814298548,0.20803111085057,-1.08333333333333));
#41305=CARTESIAN_POINT('Ctrl Pts',(-14.2484814298548,0.208031110850584,
-1.08333333333333));
#41306=CARTESIAN_POINT('Ctrl Pts',(-14.2468058395578,0.322795758952019,
-0.725928647976579));
#41307=CARTESIAN_POINT('Ctrl Pts',(-14.2449910310593,0.37779693624925,-0.352039859176988));
#41308=CARTESIAN_POINT('Ctrl Pts',(-14.2449910310593,0.37779693624925,2.46631154156404E-15));
#41309=CARTESIAN_POINT('Ctrl Pts',(-14.2449910310593,0.37779693624925,0.352039859176994));
#41310=CARTESIAN_POINT('Ctrl Pts',(-14.2468058395578,0.322795758952019,
0.725928647976587));
#41311=CARTESIAN_POINT('Ctrl Pts',(-14.2484814298548,0.208031110850583,
1.08333333333334));
#41312=CARTESIAN_POINT('',(-15.1423033840733,-0.0114224867028862,-1.08333333333333));
#41313=CARTESIAN_POINT('Origin',(-13.892722748591,-3.17092330887754,-1.08333333333333));
#41314=CARTESIAN_POINT('',(-15.1423033840733,-0.0114224867028857,1.08333333333334));
#41315=CARTESIAN_POINT('Ctrl Pts',(-15.1423033840733,-0.0114224867028744,
1.08333333333334));
#41316=CARTESIAN_POINT('Ctrl Pts',(-15.1423953499066,0.110492695607543,
0.727666221822802));
#41317=CARTESIAN_POINT('Ctrl Pts',(-15.1413590080604,0.169498193350012,
0.352782973842781));
#41318=CARTESIAN_POINT('Ctrl Pts',(-15.1413590080604,0.169498193350012,
2.67362166230902E-15));
#41319=CARTESIAN_POINT('Ctrl Pts',(-15.1413590080604,0.169498193350012,
-0.352782973842774));
#41320=CARTESIAN_POINT('Ctrl Pts',(-15.1423953499066,0.110492695607543,
-0.727666221822795));
#41321=CARTESIAN_POINT('Ctrl Pts',(-15.1423033840733,-0.0114224867028733,
-1.08333333333333));
#41322=CARTESIAN_POINT('Origin',(-13.892722748591,-3.17092330887753,1.08333333333334));
#41323=CARTESIAN_POINT('',(-13.0227870731057,-2.97236616780882,-3.45272288248773));
#41324=CARTESIAN_POINT('Origin',(-13.0227870731057,-2.97236616780882,2.99978307628674E-15));
#41325=CARTESIAN_POINT('',(-14.7626584240763,-3.36948044994625,-3.45272288248773));
#41326=CARTESIAN_POINT('Origin',(-14.7626584240763,-3.36948044994625,3.40056031423578E-15));
#41327=CARTESIAN_POINT('Origin',(-6.18284328242512,-12.8388063676095,4.97613300162231E-15));
#41328=CARTESIAN_POINT('',(-6.57000108040694,-13.6427478189686,3.96060240207311));
#41329=CARTESIAN_POINT('Origin',(-6.57000108040694,-13.6427478189686,5.28772891427451E-15));
#41330=CARTESIAN_POINT('',(-5.79568548444331,-12.0348649162504,3.96060240207311));
#41331=CARTESIAN_POINT('Origin',(-6.18284328242512,-12.8388063676095,2.51985201161581));
#41332=CARTESIAN_POINT('Origin',(-5.79568548444331,-12.0348649162504,4.66453708897012E-15));
#41333=CARTESIAN_POINT('',(-2.35859284151935,-14.0534529496467,-1.08333333333333));
#41334=CARTESIAN_POINT('',(-2.69569375163562,-14.9004267538186,-1.08333333333333));
#41335=CARTESIAN_POINT('Ctrl Pts',(-2.35859284151934,-14.0534529496467,
-1.08333333333333));
#41336=CARTESIAN_POINT('Ctrl Pts',(-2.37682723618162,-14.2398470420046,
-1.08333333333333));
#41337=CARTESIAN_POINT('Ctrl Pts',(-2.43502529011671,-14.4435268961719,
-1.08333333333332));
#41338=CARTESIAN_POINT('Ctrl Pts',(-2.56051322547963,-14.7041052789647,
-1.08333333333333));
#41339=CARTESIAN_POINT('Ctrl Pts',(-2.62287825309305,-14.806702452812,-1.08333333333333));
#41340=CARTESIAN_POINT('Ctrl Pts',(-2.69569375163558,-14.9004267538186,
-1.08333333333333));
#41341=CARTESIAN_POINT('',(-2.69569375163563,-14.9004267538187,1.08333333333334));
#41342=CARTESIAN_POINT('Ctrl Pts',(-2.69569375163559,-14.9004267538186,
1.08333333333335));
#41343=CARTESIAN_POINT('Ctrl Pts',(-2.65857154890325,-14.9071426748862,
0.955915065626573));
#41344=CARTESIAN_POINT('Ctrl Pts',(-2.628016775001,-14.9125315333598,0.826701571450498));
#41345=CARTESIAN_POINT('Ctrl Pts',(-2.60415669762586,-14.9166970252376,
0.696211209492072));
#41346=CARTESIAN_POINT('Ctrl Pts',(-2.58067270588166,-14.9207968600927,
0.567777653525379));
#41347=CARTESIAN_POINT('Ctrl Pts',(-2.56367395385075,-14.923711651889,0.438107164856101));
#41348=CARTESIAN_POINT('Ctrl Pts',(-2.55327224255806,-14.9254910506792,
0.307693975181385));
#41349=CARTESIAN_POINT('Ctrl Pts',(-2.54512176981446,-14.9268853348437,
0.205506064179128));
#41350=CARTESIAN_POINT('Ctrl Pts',(-2.54102158203148,-14.9275815713119,
0.102862147740959));
#41351=CARTESIAN_POINT('Ctrl Pts',(-2.54102158203148,-14.9275815713119,
4.44089209850063E-15));
#41352=CARTESIAN_POINT('Ctrl Pts',(-2.54102158203148,-14.9275815713119,
-0.130666807305524));
#41353=CARTESIAN_POINT('Ctrl Pts',(-2.54764001565181,-14.9264594186595,
-0.261069786498646));
#41354=CARTESIAN_POINT('Ctrl Pts',(-2.56079607270382,-14.9242020129234,
-0.390710450870999));
#41355=CARTESIAN_POINT('Ctrl Pts',(-2.57411009834303,-14.9219175018628,
-0.521907748246163));
#41356=CARTESIAN_POINT('Ctrl Pts',(-2.59411972995703,-14.9184702682937,
-0.652324314224157));
#41357=CARTESIAN_POINT('Ctrl Pts',(-2.62073179377387,-14.9137938537994,
-0.781443489202868));
#41358=CARTESIAN_POINT('Ctrl Pts',(-2.64165463403551,-14.9101171801624,
-0.882959098491507));
#41359=CARTESIAN_POINT('Ctrl Pts',(-2.66665850662476,-14.9056796321318,
-0.983672743459509));
#41360=CARTESIAN_POINT('Ctrl Pts',(-2.69569375163559,-14.9004267538186,
-1.08333333333334));
#41361=CARTESIAN_POINT('',(-2.35859284151935,-14.0534529496467,1.08333333333334));
#41362=CARTESIAN_POINT('Ctrl Pts',(-2.35859284151934,-14.0534529496467,
1.08333333333333));
#41363=CARTESIAN_POINT('Ctrl Pts',(-2.37688304383397,-14.2404175142851,
1.08333333333333));
#41364=CARTESIAN_POINT('Ctrl Pts',(-2.43503901504648,-14.4435553962822,
1.08333333333334));
#41365=CARTESIAN_POINT('Ctrl Pts',(-2.56054033827446,-14.7041615792632,
1.08333333333334));
#41366=CARTESIAN_POINT('Ctrl Pts',(-2.62284674626764,-14.8066618988743,
1.08333333333334));
#41367=CARTESIAN_POINT('Ctrl Pts',(-2.69569375163563,-14.9004267538187,
1.08333333333334));
#41368=CARTESIAN_POINT('Ctrl Pts',(-2.35859284151935,-14.0534529496467,
-1.08333333333333));
#41369=CARTESIAN_POINT('Ctrl Pts',(-2.32474809698527,-14.0591331175362,
-0.949622058007895));
#41370=CARTESIAN_POINT('Ctrl Pts',(-2.29723964086638,-14.0636285445206,
-0.814376693553736));
#41371=CARTESIAN_POINT('Ctrl Pts',(-2.27611794897253,-14.0670461391994,
-0.678132403728853));
#41372=CARTESIAN_POINT('Ctrl Pts',(-2.25509664145098,-14.0704474911881,
-0.542535637671543));
#41373=CARTESIAN_POINT('Ctrl Pts',(-2.24040145926613,-14.0727812605466,
-0.405949418799629));
#41374=CARTESIAN_POINT('Ctrl Pts',(-2.23207311688321,-14.0741020886196,
-0.268901316712528));
#41375=CARTESIAN_POINT('Ctrl Pts',(-2.22663511068775,-14.0749645256946,
-0.179415511019263));
#41376=CARTESIAN_POINT('Ctrl Pts',(-2.2239114043034,-14.075394064317,-0.0897327832369026));
#41377=CARTESIAN_POINT('Ctrl Pts',(-2.2239114043034,-14.075394064317,8.43769498715119E-15));
#41378=CARTESIAN_POINT('Ctrl Pts',(-2.2239114043034,-14.075394064317,0.137573936980349));
#41379=CARTESIAN_POINT('Ctrl Pts',(-2.23031275616482,-14.0743870796481,
0.274951212619667));
#41380=CARTESIAN_POINT('Ctrl Pts',(-2.24306143269717,-14.0723550057958,
0.411612406214657));
#41381=CARTESIAN_POINT('Ctrl Pts',(-2.25590874866049,-14.0703072093226,
0.549330978772813));
#41382=CARTESIAN_POINT('Ctrl Pts',(-2.27520203478074,-14.0672183663696,
0.68632234543694));
#41383=CARTESIAN_POINT('Ctrl Pts',(-2.30087730766032,-14.0630175856782,
0.822054935347292));
#41384=CARTESIAN_POINT('Ctrl Pts',(-2.31746020132759,-14.0603044266067,
0.909720570537337));
#41385=CARTESIAN_POINT('Ctrl Pts',(-2.33670515605249,-14.0571263627534,
0.996861109122898));
#41386=CARTESIAN_POINT('Ctrl Pts',(-2.35859284151935,-14.0534529496467,
1.08333333333334));
#41387=CARTESIAN_POINT('',(-9.96888517526507,-11.3978423664701,-1.08333333333333));
#41388=CARTESIAN_POINT('',(-9.516873369993,-10.6062067328295,-1.08333333333333));
#41389=CARTESIAN_POINT('Ctrl Pts',(-9.96888517526507,-11.3978423664701,
-1.08333333333333));
#41390=CARTESIAN_POINT('Ctrl Pts',(-9.94100828682427,-11.282476771434,-1.08333333333333));
#41391=CARTESIAN_POINT('Ctrl Pts',(-9.89967854500783,-11.1697495378475,
-1.08333333333333));
#41392=CARTESIAN_POINT('Ctrl Pts',(-9.77419060964491,-10.9091711550547,
-1.08333333333333));
#41393=CARTESIAN_POINT('Ctrl Pts',(-9.65123318042897,-10.7366777723525,
-1.08333333333333));
#41394=CARTESIAN_POINT('Ctrl Pts',(-9.51687336999256,-10.6062067328299,
-1.08333333333333));
#41395=CARTESIAN_POINT('',(-9.51687336999906,-10.6062067328363,1.08333333333334));
#41396=CARTESIAN_POINT('Ctrl Pts',(-9.51687336999256,-10.6062067328299,
1.08333333333319));
#41397=CARTESIAN_POINT('Ctrl Pts',(-9.54248335115827,-10.5832270800755,
0.949270311030248));
#41398=CARTESIAN_POINT('Ctrl Pts',(-9.56321910180067,-10.5644593135702,
0.813521288367661));
#41399=CARTESIAN_POINT('Ctrl Pts',(-9.57910097474595,-10.5500390764974,
0.676607052100613));
#41400=CARTESIAN_POINT('Ctrl Pts',(-9.59267821366648,-10.5377113740467,
0.559560573777554));
#41401=CARTESIAN_POINT('Ctrl Pts',(-9.6027075928823,-10.5285603838747,0.44166251627891));
#41402=CARTESIAN_POINT('Ctrl Pts',(-9.6091818848891,-10.5226481221753,0.323238258334718));
#41403=CARTESIAN_POINT('Ctrl Pts',(-9.61666296645239,-10.5158164698571,
0.186398348762648));
#41404=CARTESIAN_POINT('Ctrl Pts',(-9.61937600851194,-10.5133302394117,
0.0492519096262118));
#41405=CARTESIAN_POINT('Ctrl Pts',(-9.61735300288125,-10.5151805128572,
-0.08767582706605));
#41406=CARTESIAN_POINT('Ctrl Pts',(-9.61532413250719,-10.5170361502911,
-0.225000520654331));
#41407=CARTESIAN_POINT('Ctrl Pts',(-9.60853168799772,-10.5232534570122,
-0.362105241912796));
#41408=CARTESIAN_POINT('Ctrl Pts',(-9.59697252030892,-10.5337846211338,
-0.498460177595657));
#41409=CARTESIAN_POINT('Ctrl Pts',(-9.5853634847053,-10.5443612182148,-0.635403368116659));
#41410=CARTESIAN_POINT('Ctrl Pts',(-9.56894645381043,-10.5592890006364,
-0.771590289741169));
#41411=CARTESIAN_POINT('Ctrl Pts',(-9.54768316346852,-10.578480335569,-0.906484242526434));
#41412=CARTESIAN_POINT('Ctrl Pts',(-9.53834928383367,-10.5869046954593,
-0.965698216399696));
#41413=CARTESIAN_POINT('Ctrl Pts',(-9.52808112091929,-10.5961500981613,
-1.02466304565381));
#41414=CARTESIAN_POINT('Ctrl Pts',(-9.51687336999256,-10.6062067328299,
-1.08333333333318));
#41415=CARTESIAN_POINT('',(-9.96888517526507,-11.3978423664701,1.08333333333334));
#41416=CARTESIAN_POINT('Ctrl Pts',(-9.96888517526507,-11.3978423664701,
1.08333333333333));
#41417=CARTESIAN_POINT('Ctrl Pts',(-9.94100828682427,-11.282476771434,1.08333333333333));
#41418=CARTESIAN_POINT('Ctrl Pts',(-9.89967854500783,-11.1697495378475,
1.08333333333333));
#41419=CARTESIAN_POINT('Ctrl Pts',(-9.77419060964618,-10.9091711550573,
1.08333333333333));
#41420=CARTESIAN_POINT('Ctrl Pts',(-9.6512331804331,-10.7366777723579,1.08333333333333));
#41421=CARTESIAN_POINT('Ctrl Pts',(-9.51687336999908,-10.6062067328363,
1.08333333333333));
#41422=CARTESIAN_POINT('Ctrl Pts',(-9.96888517526508,-11.3978423664701,
-1.08333333333333));
#41423=CARTESIAN_POINT('Ctrl Pts',(-9.99706424266063,-11.3731961327199,
-0.956888632103256));
#41424=CARTESIAN_POINT('Ctrl Pts',(-10.020155672713,-11.3528209383891,-0.828820583351071));
#41425=CARTESIAN_POINT('Ctrl Pts',(-10.038197564346,-11.3368457653652,-0.699646919261599));
#41426=CARTESIAN_POINT('Ctrl Pts',(-10.0561445912219,-11.3209545902358,
-0.571152453812953));
#41427=CARTESIAN_POINT('Ctrl Pts',(-10.0690951385517,-11.3094172714603,
-0.441563969171296));
#41428=CARTESIAN_POINT('Ctrl Pts',(-10.0770534136919,-11.3023217413999,
-0.311391073637437));
#41429=CARTESIAN_POINT('Ctrl Pts',(-10.0849478229272,-11.2952831536342,
-0.182262827807044));
#41430=CARTESIAN_POINT('Ctrl Pts',(-10.0879298097314,-11.2926153440655,
-0.0525595133516554));
#41431=CARTESIAN_POINT('Ctrl Pts',(-10.0859696068728,-11.2943658227348,
0.0772214321950453));
#41432=CARTESIAN_POINT('Ctrl Pts',(-10.0846326712896,-11.2955597181575,
0.165737150534751));
#41433=CARTESIAN_POINT('Ctrl Pts',(-10.0809960349672,-11.2988081152181,
0.2542889811304));
#41434=CARTESIAN_POINT('Ctrl Pts',(-10.0750409796764,-11.304115688826,0.342719102199531));
#41435=CARTESIAN_POINT('Ctrl Pts',(-10.0660632343107,-11.3121173012435,
0.476034927301883));
#41436=CARTESIAN_POINT('Ctrl Pts',(-10.0518705086679,-11.3247537742305,
0.608312350206005));
#41437=CARTESIAN_POINT('Ctrl Pts',(-10.0325330571073,-11.3418588735079,
0.739057191238004));
#41438=CARTESIAN_POINT('Ctrl Pts',(-10.0153642561251,-11.3570456753652,
0.855139299994515));
#41439=CARTESIAN_POINT('Ctrl Pts',(-9.99413932000721,-11.3757543553326,
0.970013302477919));
#41440=CARTESIAN_POINT('Ctrl Pts',(-9.96888517526508,-11.3978423664701,
1.08333333333334));
#41441=CARTESIAN_POINT('Origin',(-6.18284328242512,-12.8388063676095,4.97613300162231E-15));
#41442=CARTESIAN_POINT('',(-3.38061559238688,-14.7601124814492,1.08333333333334));
#41443=CARTESIAN_POINT('',(-3.12168342103518,-14.3129832609672,1.08333333333334));
#41444=CARTESIAN_POINT('Origin',(-6.18284328242512,-12.8388063676095,1.08333333333334));
#41445=CARTESIAN_POINT('',(-3.38061559238688,-14.7601124814492,-1.08333333333333));
#41446=CARTESIAN_POINT('Ctrl Pts',(-3.38061559238688,-14.7601124814492,
-1.08333333333333));
#41447=CARTESIAN_POINT('Ctrl Pts',(-3.26177754255684,-14.7873308217382,
-0.727666221822789));
#41448=CARTESIAN_POINT('Ctrl Pts',(-3.20402082808,-14.799450421612,-0.35278297384277));
#41449=CARTESIAN_POINT('Ctrl Pts',(-3.20402082808,-14.799450421612,0.352782973842781));
#41450=CARTESIAN_POINT('Ctrl Pts',(-3.26177754255684,-14.7873308217382,
0.727666221822798));
#41451=CARTESIAN_POINT('Ctrl Pts',(-3.38061559238688,-14.7601124814492,
1.08333333333334));
#41452=CARTESIAN_POINT('',(-2.96777005865995,-13.9375335292483,-1.08333333333333));
#41453=CARTESIAN_POINT('Origin',(-6.18284328242512,-12.8388063676095,-1.08333333333333));
#41454=CARTESIAN_POINT('',(-2.96777005865995,-13.9375335292483,1.08333333333334));
#41455=CARTESIAN_POINT('Ctrl Pts',(-2.96777005865994,-13.9375335292483,
1.08333333333334));
#41456=CARTESIAN_POINT('Ctrl Pts',(-2.85550994597631,-13.9614374861791,
0.725928647976589));
#41457=CARTESIAN_POINT('Ctrl Pts',(-2.80148393014434,-13.9719070920595,
0.352039859176996));
#41458=CARTESIAN_POINT('Ctrl Pts',(-2.80148393014434,-13.9719070920595,
-0.352039859176986));
#41459=CARTESIAN_POINT('Ctrl Pts',(-2.85550994597631,-13.9614374861791,
-0.725928647976579));
#41460=CARTESIAN_POINT('Ctrl Pts',(-2.96777005865994,-13.9375335292483,
-1.08333333333333));
#41461=CARTESIAN_POINT('Origin',(-6.18284328242512,-12.8388063676095,1.08333333333334));
#41462=CARTESIAN_POINT('',(-9.24400314381506,-11.3646294742518,1.08333333333334));
#41463=CARTESIAN_POINT('Origin',(-6.18284328242512,-12.8388063676095,4.97613300162231E-15));
#41464=CARTESIAN_POINT('',(-9.04642813528379,-11.0102060831369,1.08333333333334));
#41465=CARTESIAN_POINT('Origin',(-6.18284328242512,-12.8388063676095,1.08333333333334));
#41466=CARTESIAN_POINT('',(-9.04642813528379,-11.0102060831369,-1.08333333333333));
#41467=CARTESIAN_POINT('Ctrl Pts',(-9.0464281352838,-11.0102060831369,-1.08333333333332));
#41468=CARTESIAN_POINT('Ctrl Pts',(-9.13511003678158,-10.9373414661859,
-0.725928647976569));
#41469=CARTESIAN_POINT('Ctrl Pts',(-9.17698017417422,-10.901629918632,-0.352039859176982));
#41470=CARTESIAN_POINT('Ctrl Pts',(-9.17698017417422,-10.901629918632,4.5383086406711E-15));
#41471=CARTESIAN_POINT('Ctrl Pts',(-9.17698017417422,-10.901629918632,0.352039859176991));
#41472=CARTESIAN_POINT('Ctrl Pts',(-9.13511003678158,-10.9373414661859,
0.725928647976579));
#41473=CARTESIAN_POINT('Ctrl Pts',(-9.0464281352838,-11.0102060831369,1.08333333333333));
#41474=CARTESIAN_POINT('',(-9.43214127690829,-11.8458513067218,-1.08333333333333));
#41475=CARTESIAN_POINT('Origin',(-6.18284328242512,-12.8388063676095,-1.08333333333333));
#41476=CARTESIAN_POINT('',(-9.43214127690829,-11.8458513067218,1.08333333333334));
#41477=CARTESIAN_POINT('Ctrl Pts',(-9.43214127690829,-11.8458513067218,
1.08333333333333));
#41478=CARTESIAN_POINT('Ctrl Pts',(-9.52751574438859,-11.7699103356433,
0.727666221822793));
#41479=CARTESIAN_POINT('Ctrl Pts',(-9.57300195158999,-11.7323107648653,
0.352782973842778));
#41480=CARTESIAN_POINT('Ctrl Pts',(-9.57300195158999,-11.7323107648653,
4.85994849902029E-15));
#41481=CARTESIAN_POINT('Ctrl Pts',(-9.57300195158999,-11.7323107648653,
-0.352782973842768));
#41482=CARTESIAN_POINT('Ctrl Pts',(-9.52751574438859,-11.7699103356433,
-0.727666221822784));
#41483=CARTESIAN_POINT('Ctrl Pts',(-9.43214127690829,-11.8458513067218,
-1.08333333333332));
#41484=CARTESIAN_POINT('Origin',(-6.18284328242512,-12.8388063676095,1.08333333333334));
#41485=CARTESIAN_POINT('',(-5.79568548444331,-12.0348649162504,-3.45272288248773));
#41486=CARTESIAN_POINT('Origin',(-5.79568548444331,-12.0348649162504,4.66453708897012E-15));
#41487=CARTESIAN_POINT('',(-6.57000108040694,-13.6427478189686,-3.45272288248772));
#41488=CARTESIAN_POINT('Origin',(-6.57000108040694,-13.6427478189686,5.28772891427451E-15));
#41489=CARTESIAN_POINT('Origin',(6.1828432824253,-12.8388063676094,4.9761330016223E-15));
#41490=CARTESIAN_POINT('',(6.57000108040713,-13.6427478189685,3.96060240207311));
#41491=CARTESIAN_POINT('Origin',(6.57000108040713,-13.6427478189685,5.28772891427449E-15));
#41492=CARTESIAN_POINT('',(5.79568548444348,-12.0348649162503,3.96060240207311));
#41493=CARTESIAN_POINT('Origin',(6.1828432824253,-12.8388063676094,2.51985201161581));
#41494=CARTESIAN_POINT('Origin',(5.79568548444348,-12.0348649162504,4.66453708897011E-15));
#41495=CARTESIAN_POINT('',(9.51687336999268,-10.6062067328298,-1.08333333333333));
#41496=CARTESIAN_POINT('',(9.96888517526453,-11.3978423664706,-1.08333333333333));
#41497=CARTESIAN_POINT('Ctrl Pts',(9.5168733699927,-10.6062067328298,-1.08333333333333));
#41498=CARTESIAN_POINT('Ctrl Pts',(9.65164439811578,-10.737077088181,-1.08333333333333));
#41499=CARTESIAN_POINT('Ctrl Pts',(9.77420433457484,-10.9091996551649,-1.08333333333333));
#41500=CARTESIAN_POINT('Ctrl Pts',(9.89970565780286,-11.169805838146,-1.08333333333333));
#41501=CARTESIAN_POINT('Ctrl Pts',(9.94099622466366,-11.2824268534395,-1.08333333333333));
#41502=CARTESIAN_POINT('Ctrl Pts',(9.96888517526534,-11.3978423664704,-1.08333333333333));
#41503=CARTESIAN_POINT('',(9.9688851752657,-11.3978423664719,1.08333333333334));
#41504=CARTESIAN_POINT('Ctrl Pts',(9.96888517526519,-11.39784236647,1.08333333333359));
#41505=CARTESIAN_POINT('Ctrl Pts',(9.99728120861575,-11.3730063679711,0.955915065626921));
#41506=CARTESIAN_POINT('Ctrl Pts',(10.0205449777511,-11.3524775820965,0.826701571450959));
#41507=CARTESIAN_POINT('Ctrl Pts',(10.038678205356,-11.3364201641361,0.696211209492648));
#41508=CARTESIAN_POINT('Ctrl Pts',(10.0565256146782,-11.3206158452779,0.567777653525928));
#41509=CARTESIAN_POINT('Ctrl Pts',(10.0694030392049,-11.309143028737,0.438107164856624));
#41510=CARTESIAN_POINT('Ctrl Pts',(10.0772795901119,-11.3021200803759,0.307693975181881));
#41511=CARTESIAN_POINT('Ctrl Pts',(10.0834514220032,-11.2966171061454,0.20550606417946));
#41512=CARTESIAN_POINT('Ctrl Pts',(10.0865521868617,-11.2938455465903,0.102862147741125));
#41513=CARTESIAN_POINT('Ctrl Pts',(10.0865521868617,-11.2938455465903,4.44089209850063E-15));
#41514=CARTESIAN_POINT('Ctrl Pts',(10.0865521868617,-11.2938455465903,-0.130666807305562));
#41515=CARTESIAN_POINT('Ctrl Pts',(10.0815483267233,-11.2983203956244,-0.261069786498721));
#41516=CARTESIAN_POINT('Ctrl Pts',(10.0715807484455,-11.3071987457576,-0.390710450871112));
#41517=CARTESIAN_POINT('Ctrl Pts',(10.0614934865685,-11.3161837008123,-0.521907748246463));
#41518=CARTESIAN_POINT('Ctrl Pts',(10.0463225295865,-11.3296785457857,-0.652324314224642));
#41519=CARTESIAN_POINT('Ctrl Pts',(10.0260740111135,-11.3475689983448,-0.781443489203535));
#41520=CARTESIAN_POINT('Ctrl Pts',(10.0101542943843,-11.3616347650465,-0.88295909849203));
#41521=CARTESIAN_POINT('Ctrl Pts',(9.99109522006272,-11.3784168138781,-0.983672743459888));
#41522=CARTESIAN_POINT('Ctrl Pts',(9.96888517526519,-11.39784236647,-1.08333333333358));
#41523=CARTESIAN_POINT('',(9.51687336999268,-10.6062067328298,1.08333333333334));
#41524=CARTESIAN_POINT('Ctrl Pts',(9.5168733699927,-10.6062067328298,1.08333333333333));
#41525=CARTESIAN_POINT('Ctrl Pts',(9.65123318042911,-10.7366777723523,1.08333333333333));
#41526=CARTESIAN_POINT('Ctrl Pts',(9.77419060964506,-10.9091711550545,1.08333333333333));
#41527=CARTESIAN_POINT('Ctrl Pts',(9.89967854500826,-11.1697495378479,1.08333333333333));
#41528=CARTESIAN_POINT('Ctrl Pts',(9.94100828682489,-11.2824767714351,1.08333333333333));
#41529=CARTESIAN_POINT('Ctrl Pts',(9.96888517526571,-11.3978423664719,1.08333333333333));
#41530=CARTESIAN_POINT('Ctrl Pts',(9.51687336999268,-10.6062067328298,-1.08333333333333));
#41531=CARTESIAN_POINT('Ctrl Pts',(9.54241615713793,-10.5832873727889,-0.949622058007762));
#41532=CARTESIAN_POINT('Ctrl Pts',(9.56308206533645,-10.5645832486408,-0.814376693553466));
#41533=CARTESIAN_POINT('Ctrl Pts',(9.5789232079445,-10.5502004803844,-0.678132403728444));
#41534=CARTESIAN_POINT('Ctrl Pts',(9.59468906287363,-10.5358860686389,-0.542535637671145));
#41535=CARTESIAN_POINT('Ctrl Pts',(9.60567597345963,-10.5258519939611,-0.405949418799242));
#41536=CARTESIAN_POINT('Ctrl Pts',(9.61190127497217,-10.5201641565229,-0.268901316712153));
#41537=CARTESIAN_POINT('Ctrl Pts',(9.61596609683434,-10.5164502727984,-0.179415511019018));
#41538=CARTESIAN_POINT('Ctrl Pts',(9.61800012680612,-10.5145886063487,-0.0897327832367887));
#41539=CARTESIAN_POINT('Ctrl Pts',(9.61800012680612,-10.5145886063487,-9.32587340685131E-15));
#41540=CARTESIAN_POINT('Ctrl Pts',(9.61800012680612,-10.5145886063487,0.137573936980381));
#41541=CARTESIAN_POINT('Ctrl Pts',(9.61322165688595,-10.5189655400926,0.274951212619743));
#41542=CARTESIAN_POINT('Ctrl Pts',(9.6036842477684,-10.5276658794419,0.411612406214774));
#41543=CARTESIAN_POINT('Ctrl Pts',(9.59407304553156,-10.5364335353099,0.54933097877281));
#41544=CARTESIAN_POINT('Ctrl Pts',(9.57962892372621,-10.5495917717182,0.686322345436814));
#41545=CARTESIAN_POINT('Ctrl Pts',(9.5603363503304,-10.5670463644555,0.822054935347047));
#41546=CARTESIAN_POINT('Ctrl Pts',(9.54787585206456,-10.5783197657831,0.909720570537174));
#41547=CARTESIAN_POINT('Ctrl Pts',(9.5333921086825,-10.5913845868635,0.996861109122817));
#41548=CARTESIAN_POINT('Ctrl Pts',(9.51687336999268,-10.6062067328298,1.08333333333334));
#41549=CARTESIAN_POINT('',(2.69569375163578,-14.9004267538186,-1.08333333333333));
#41550=CARTESIAN_POINT('',(2.35859284151893,-14.0534529496468,-1.08333333333333));
#41551=CARTESIAN_POINT('Ctrl Pts',(2.6956937516358,-14.9004267538186,-1.08333333333332));
#41552=CARTESIAN_POINT('Ctrl Pts',(2.62284674626782,-14.8066618988742,-1.08333333333332));
#41553=CARTESIAN_POINT('Ctrl Pts',(2.56054033827465,-14.7041615792632,-1.08333333333332));
#41554=CARTESIAN_POINT('Ctrl Pts',(2.4350390150467,-14.4435553962822,-1.08333333333332));
#41555=CARTESIAN_POINT('Ctrl Pts',(2.37688304383419,-14.2404175142851,-1.08333333333332));
#41556=CARTESIAN_POINT('Ctrl Pts',(2.35859284151955,-14.0534529496467,-1.08333333333332));
#41557=CARTESIAN_POINT('',(2.35859284152043,-14.0534529496557,1.08333333333334));
#41558=CARTESIAN_POINT('Ctrl Pts',(2.35859284151951,-14.0534529496467,1.08333333333319));
#41559=CARTESIAN_POINT('Ctrl Pts',(2.32465906345733,-14.0591480600448,0.949270311030372));
#41560=CARTESIAN_POINT('Ctrl Pts',(2.29705730368849,-14.0636584116899,0.813521288367913));
#41561=CARTESIAN_POINT('Ctrl Pts',(2.27588092254449,-14.0670844892038,0.676607052100994));
#41562=CARTESIAN_POINT('Ctrl Pts',(2.25777746665768,-14.0700134052785,0.55956057377781));
#41563=CARTESIAN_POINT('Ctrl Pts',(2.24436971878542,-14.0721491406499,0.441662516279038));
#41564=CARTESIAN_POINT('Ctrl Pts',(2.23571067141573,-14.073524711092,0.323238258334718));
#41565=CARTESIAN_POINT('Ctrl Pts',(2.2257050924945,-14.0751141906309,0.186398348762649));
#41566=CARTESIAN_POINT('Ctrl Pts',(2.22206972520347,-14.0756851929985,0.0492519096262131));
#41567=CARTESIAN_POINT('Ctrl Pts',(2.22477765061414,-14.0752571701311,-0.087675827066048));
#41568=CARTESIAN_POINT('Ctrl Pts',(2.22749342636756,-14.0748279064149,-0.225000520654297));
#41569=CARTESIAN_POINT('Ctrl Pts',(2.23658933237962,-14.0733937867901,-0.362105241912729));
#41570=CARTESIAN_POINT('Ctrl Pts',(2.25202995120888,-14.0709225390114,-0.498460177595558));
#41571=CARTESIAN_POINT('Ctrl Pts',(2.26753718309241,-14.0684406299137,-0.635403368116538));
#41572=CARTESIAN_POINT('Ctrl Pts',(2.28944404469282,-14.0649125984157,-0.771590289741026));
#41573=CARTESIAN_POINT('Ctrl Pts',(2.31770587921582,-14.0602538902201,-0.906484242526269));
#41574=CARTESIAN_POINT('Ctrl Pts',(2.33011188776182,-14.0582088717468,-0.965698216399587));
#41575=CARTESIAN_POINT('Ctrl Pts',(2.34374232952329,-14.0559453130119,-1.02466304565376));
#41576=CARTESIAN_POINT('Ctrl Pts',(2.35859284151951,-14.0534529496467,-1.08333333333318));
#41577=CARTESIAN_POINT('',(2.69569375163578,-14.9004267538186,1.08333333333334));
#41578=CARTESIAN_POINT('Ctrl Pts',(2.6956937516358,-14.9004267538186,1.08333333333334));
#41579=CARTESIAN_POINT('Ctrl Pts',(2.62284674626782,-14.8066618988742,1.08333333333334));
#41580=CARTESIAN_POINT('Ctrl Pts',(2.56054033827465,-14.7041615792632,1.08333333333334));
#41581=CARTESIAN_POINT('Ctrl Pts',(2.43503901504795,-14.4435553962848,1.08333333333334));
#41582=CARTESIAN_POINT('Ctrl Pts',(2.37688304383586,-14.2404175142916,1.08333333333334));
#41583=CARTESIAN_POINT('Ctrl Pts',(2.35859284152042,-14.0534529496557,1.08333333333334));
#41584=CARTESIAN_POINT('Ctrl Pts',(2.69569375163578,-14.9004267538186,-1.08333333333333));
#41585=CARTESIAN_POINT('Ctrl Pts',(2.65885518901859,-14.9070913604575,-0.956888632103347));
#41586=CARTESIAN_POINT('Ctrl Pts',(2.62852794948137,-14.9124412415715,-0.828820583351256));
#41587=CARTESIAN_POINT('Ctrl Pts',(2.60478912083403,-14.9165866029902,-0.699646919261879));
#41588=CARTESIAN_POINT('Ctrl Pts',(2.58117511159368,-14.9207101679857,-0.571152453813268));
#41589=CARTESIAN_POINT('Ctrl Pts',(2.56408033836306,-14.9236419130061,-0.441563969171648));
#41590=CARTESIAN_POINT('Ctrl Pts',(2.55357092618676,-14.9254399524253,-0.311391073637824));
#41591=CARTESIAN_POINT('Ctrl Pts',(2.54314585302948,-14.9272235624095,-0.182262827807427));
#41592=CARTESIAN_POINT('Ctrl Pts',(2.53920083715778,-14.927891621514,-0.0525595133520343));
#41593=CARTESIAN_POINT('Ctrl Pts',(2.54179158298272,-14.9274504788058,0.077221432194672));
#41594=CARTESIAN_POINT('Ctrl Pts',(2.54355857371286,-14.9271496020974,0.165737150534507));
#41595=CARTESIAN_POINT('Ctrl Pts',(2.54836567846244,-14.9263317077699,0.254288981130285));
#41596=CARTESIAN_POINT('Ctrl Pts',(2.55622822284789,-14.9249850760809,0.342719102199546));
#41597=CARTESIAN_POINT('Ctrl Pts',(2.56808166802554,-14.9229549158531,0.47603492730158));
#41598=CARTESIAN_POINT('Ctrl Pts',(2.58681028013297,-14.9197373081624,0.608312350205393));
#41599=CARTESIAN_POINT('Ctrl Pts',(2.61224028910069,-14.9152835347009,0.739057191237091));
#41600=CARTESIAN_POINT('Ctrl Pts',(2.63481838123332,-14.9113292416576,0.855139299993913));
#41601=CARTESIAN_POINT('Ctrl Pts',(2.66267894744191,-14.9063995895532,0.970013302477622));
#41602=CARTESIAN_POINT('Ctrl Pts',(2.69569375163578,-14.9004267538186,1.08333333333334));
#41603=CARTESIAN_POINT('Origin',(6.1828432824253,-12.8388063676094,4.9761330016223E-15));
#41604=CARTESIAN_POINT('',(9.43214127690845,-11.8458513067217,1.08333333333334));
#41605=CARTESIAN_POINT('',(9.24400314381522,-11.3646294742516,1.08333333333334));
#41606=CARTESIAN_POINT('Origin',(6.1828432824253,-12.8388063676094,1.08333333333334));
#41607=CARTESIAN_POINT('',(9.43214127690845,-11.8458513067217,-1.08333333333333));
#41608=CARTESIAN_POINT('Ctrl Pts',(9.43214127690846,-11.8458513067217,-1.08333333333333));
#41609=CARTESIAN_POINT('Ctrl Pts',(9.52751574438875,-11.7699103356432,-0.727666221822791));
#41610=CARTESIAN_POINT('Ctrl Pts',(9.57300195159016,-11.7323107648652,-0.352782973842771));
#41611=CARTESIAN_POINT('Ctrl Pts',(9.57300195159016,-11.7323107648652,0.35278297384278));
#41612=CARTESIAN_POINT('Ctrl Pts',(9.52751574438876,-11.7699103356432,0.7276662218228));
#41613=CARTESIAN_POINT('Ctrl Pts',(9.43214127690846,-11.8458513067217,1.08333333333334));
#41614=CARTESIAN_POINT('',(9.04642813528394,-11.0102060831368,-1.08333333333333));
#41615=CARTESIAN_POINT('Origin',(6.1828432824253,-12.8388063676094,-1.08333333333333));
#41616=CARTESIAN_POINT('',(9.04642813528394,-11.0102060831368,1.08333333333334));
#41617=CARTESIAN_POINT('Ctrl Pts',(9.04642813528396,-11.0102060831368,1.08333333333334));
#41618=CARTESIAN_POINT('Ctrl Pts',(9.13511003678174,-10.9373414661857,0.725928647976586));
#41619=CARTESIAN_POINT('Ctrl Pts',(9.17698017417438,-10.9016299186319,0.352039859176995));
#41620=CARTESIAN_POINT('Ctrl Pts',(9.17698017417438,-10.9016299186319,-0.352039859176985));
#41621=CARTESIAN_POINT('Ctrl Pts',(9.13511003678174,-10.9373414661857,-0.725928647976577));
#41622=CARTESIAN_POINT('Ctrl Pts',(9.04642813528395,-11.0102060831368,-1.08333333333333));
#41623=CARTESIAN_POINT('Origin',(6.1828432824253,-12.8388063676094,1.08333333333334));
#41624=CARTESIAN_POINT('',(3.12168342103538,-14.3129832609672,1.08333333333334));
#41625=CARTESIAN_POINT('Origin',(6.1828432824253,-12.8388063676094,4.9761330016223E-15));
#41626=CARTESIAN_POINT('',(2.96777005866014,-13.9375335292483,1.08333333333334));
#41627=CARTESIAN_POINT('Origin',(6.1828432824253,-12.8388063676094,1.08333333333334));
#41628=CARTESIAN_POINT('',(2.96777005866014,-13.9375335292483,-1.08333333333333));
#41629=CARTESIAN_POINT('Ctrl Pts',(2.96777005866014,-13.9375335292483,-1.08333333333333));
#41630=CARTESIAN_POINT('Ctrl Pts',(2.85550994597651,-13.9614374861791,-0.725928647976576));
#41631=CARTESIAN_POINT('Ctrl Pts',(2.80148393014454,-13.9719070920595,-0.352039859176985));
#41632=CARTESIAN_POINT('Ctrl Pts',(2.80148393014454,-13.9719070920595,5.10230940761107E-15));
#41633=CARTESIAN_POINT('Ctrl Pts',(2.80148393014454,-13.9719070920595,0.352039859176993));
#41634=CARTESIAN_POINT('Ctrl Pts',(2.85550994597651,-13.9614374861791,0.725928647976584));
#41635=CARTESIAN_POINT('Ctrl Pts',(2.96777005866014,-13.9375335292483,1.08333333333333));
#41636=CARTESIAN_POINT('',(3.38061559238708,-14.7601124814491,-1.08333333333333));
#41637=CARTESIAN_POINT('Origin',(6.1828432824253,-12.8388063676094,-1.08333333333333));
#41638=CARTESIAN_POINT('',(3.38061559238708,-14.7601124814491,1.08333333333334));
#41639=CARTESIAN_POINT('Ctrl Pts',(3.3806155923871,-14.7601124814491,1.08333333333334));
#41640=CARTESIAN_POINT('Ctrl Pts',(3.26177754255705,-14.7873308217381,0.727666221822799));
#41641=CARTESIAN_POINT('Ctrl Pts',(3.20402082808022,-14.7994504216119,0.35278297384278));
#41642=CARTESIAN_POINT('Ctrl Pts',(3.20402082808022,-14.7994504216119,5.42337291349619E-15));
#41643=CARTESIAN_POINT('Ctrl Pts',(3.20402082808022,-14.7994504216119,-0.35278297384277));
#41644=CARTESIAN_POINT('Ctrl Pts',(3.26177754255705,-14.7873308217381,-0.727666221822788));
#41645=CARTESIAN_POINT('Ctrl Pts',(3.3806155923871,-14.7601124814491,-1.08333333333333));
#41646=CARTESIAN_POINT('Origin',(6.1828432824253,-12.8388063676094,1.08333333333334));
#41647=CARTESIAN_POINT('',(5.79568548444348,-12.0348649162504,-3.45272288248773));
#41648=CARTESIAN_POINT('Origin',(5.79568548444348,-12.0348649162504,4.66453708897011E-15));
#41649=CARTESIAN_POINT('',(6.57000108040713,-13.6427478189685,-3.45272288248772));
#41650=CARTESIAN_POINT('Origin',(6.57000108040713,-13.6427478189685,5.28772891427449E-15));
#41651=CARTESIAN_POINT('Origin',(13.892722748591,-3.17092330887735,3.20017169526122E-15));
#41652=CARTESIAN_POINT('',(14.7626584240763,-3.36948044994605,3.96060240207311));
#41653=CARTESIAN_POINT('Origin',(14.7626584240763,-3.36948044994605,3.40056031423575E-15));
#41654=CARTESIAN_POINT('',(13.0227870731057,-2.97236616780864,3.96060240207311));
#41655=CARTESIAN_POINT('Origin',(13.892722748591,-3.17092330887735,2.5198520116158));
#41656=CARTESIAN_POINT('Origin',(13.0227870731057,-2.97236616780865,2.9997830762867E-15));
#41657=CARTESIAN_POINT('',(14.2259398250621,0.827729480997053,-1.08333333333333));
#41658=CARTESIAN_POINT('',(15.1266902369927,0.68754979644376,-1.08333333333333));
#41659=CARTESIAN_POINT('Ctrl Pts',(14.2259398250621,0.827729480997104,-1.08333333333333));
#41660=CARTESIAN_POINT('Ctrl Pts',(14.4122867506183,0.85150138178118,-1.08333333333333));
#41661=CARTESIAN_POINT('Ctrl Pts',(14.6232724628281,0.840005933409976,-1.08333333333333));
#41662=CARTESIAN_POINT('Ctrl Pts',(14.9052713763609,0.775641521611009,-1.08333333333333));
#41663=CARTESIAN_POINT('Ctrl Pts',(15.0190662790554,0.737705732201359,-1.08333333333333));
#41664=CARTESIAN_POINT('Ctrl Pts',(15.1266902369927,0.687549796443767,-1.08333333333333));
#41665=CARTESIAN_POINT('',(15.1266902369927,0.687549796443762,1.08333333333334));
#41666=CARTESIAN_POINT('Ctrl Pts',(15.1266902369927,0.687549796443768,1.08333333333334));
#41667=CARTESIAN_POINT('Ctrl Pts',(15.1249773086751,0.725235701077452,0.955915065626868));
#41668=CARTESIAN_POINT('Ctrl Pts',(15.1234319803901,0.756223536825589,0.826701571451108));
#41669=CARTESIAN_POINT('Ctrl Pts',(15.122183667988,0.780412301388443,0.696211209493001));
#41670=CARTESIAN_POINT('Ctrl Pts',(15.1209550316477,0.804219799510377,0.567777653526322));
#41671=CARTESIAN_POINT('Ctrl Pts',(15.12001416535,0.821440959530357,0.43810716485706));
#41672=CARTESIAN_POINT('Ctrl Pts',(15.1194343523859,0.831977831684773,0.307693975182356));
#41673=CARTESIAN_POINT('Ctrl Pts',(15.1189800281283,0.840234212474528,0.205506064179778));
#41674=CARTESIAN_POINT('Ctrl Pts',(15.1187464308798,0.844386527178536,0.102862147741283));
#41675=CARTESIAN_POINT('Ctrl Pts',(15.1187464308798,0.844386527178536,1.99840144432528E-15));
#41676=CARTESIAN_POINT('Ctrl Pts',(15.1187464308798,0.844386527178536,-0.130666807305585));
#41677=CARTESIAN_POINT('Ctrl Pts',(15.1191251529677,0.837684329050871,-0.261069786498764));
#41678=CARTESIAN_POINT('Ctrl Pts',(15.1198518432089,0.824355801783881,-0.390710450871172));
#41679=CARTESIAN_POINT('Ctrl Pts',(15.1205872590302,0.810867235029882,-0.521907748246314));
#41680=CARTESIAN_POINT('Ctrl Pts',(15.1216790167187,0.790592205023559,-0.652324314224285));
#41681=CARTESIAN_POINT('Ctrl Pts',(15.1230415909943,0.763606761086929,-0.781443489202972));
#41682=CARTESIAN_POINT('Ctrl Pts',(15.1241128691977,0.742390363262186,-0.882959098491574));
#41683=CARTESIAN_POINT('Ctrl Pts',(15.1253504648421,0.717025942630064,-0.983672743459537));
#41684=CARTESIAN_POINT('Ctrl Pts',(15.1266902369927,0.687549796443768,-1.08333333333333));
#41685=CARTESIAN_POINT('',(14.2259398250621,0.827729480997055,1.08333333333334));
#41686=CARTESIAN_POINT('Ctrl Pts',(14.2259398250621,0.827729480997104,1.08333333333333));
#41687=CARTESIAN_POINT('Ctrl Pts',(14.4122867506183,0.85150138178118,1.08333333333333));
#41688=CARTESIAN_POINT('Ctrl Pts',(14.6232724628281,0.840005933409977,1.08333333333333));
#41689=CARTESIAN_POINT('Ctrl Pts',(14.9052713763609,0.775641521611009,1.08333333333333));
#41690=CARTESIAN_POINT('Ctrl Pts',(15.0190662790554,0.73770573220136,1.08333333333333));
#41691=CARTESIAN_POINT('Ctrl Pts',(15.1266902369927,0.687549796443768,1.08333333333333));
#41692=CARTESIAN_POINT('Ctrl Pts',(14.2259398250621,0.8277294809971,-1.08333333333334));
#41693=CARTESIAN_POINT('Ctrl Pts',(14.2239464151202,0.861989623387911,-0.949622058007612));
#41694=CARTESIAN_POINT('Ctrl Pts',(14.2222079250172,0.889808711690379,-0.814376693553152));
#41695=CARTESIAN_POINT('Ctrl Pts',(14.2208398148552,0.911161325030034,-0.678132403727965));
#41696=CARTESIAN_POINT('Ctrl Pts',(14.2194782068654,0.932412456504566,-0.542535637670654));
#41697=CARTESIAN_POINT('Ctrl Pts',(14.2184834780892,0.947258512328438,-0.40594941879874));
#41698=CARTESIAN_POINT('Ctrl Pts',(14.2179179597194,0.955671957676133,-0.268901316711642));
#41699=CARTESIAN_POINT('Ctrl Pts',(14.2175487034788,0.961165532006069,-0.179415511018676));
#41700=CARTESIAN_POINT('Ctrl Pts',(14.2173613909827,0.963916530720146,-0.0897327832366183));
#41701=CARTESIAN_POINT('Ctrl Pts',(14.2173613909827,0.963916530720146,-1.06581410364015E-14));
#41702=CARTESIAN_POINT('Ctrl Pts',(14.2173613909827,0.963916530720146,0.13757393698032));
#41703=CARTESIAN_POINT('Ctrl Pts',(14.2178040883167,0.957451598945758,0.274951212619625));
#41704=CARTESIAN_POINT('Ctrl Pts',(14.2186598102071,0.944570379379524,0.411612406214599));
#41705=CARTESIAN_POINT('Ctrl Pts',(14.2195221530139,0.931589494866494,0.549330978772693));
#41706=CARTESIAN_POINT('Ctrl Pts',(14.2208039138492,0.912092599491427,0.686322345436757));
#41707=CARTESIAN_POINT('Ctrl Pts',(14.222421741201,0.886126297665472,0.822054935347047));
#41708=CARTESIAN_POINT('Ctrl Pts',(14.2234666476786,0.869355437073955,0.909720570537178));
#41709=CARTESIAN_POINT('Ctrl Pts',(14.2246506698206,0.849885807807131,0.996861109122824));
#41710=CARTESIAN_POINT('Ctrl Pts',(14.2259398250621,0.827729480997101,1.08333333333335));
#41711=CARTESIAN_POINT('',(13.3303603014235,-7.18268588222768,-1.08333333333333));
#41712=CARTESIAN_POINT('',(12.4579905368411,-6.91816245718305,-1.08333333333333));
#41713=CARTESIAN_POINT('Ctrl Pts',(13.3303603014235,-7.18268588222769,-1.08333333333333));
#41714=CARTESIAN_POINT('Ctrl Pts',(13.2116326209361,-7.18117853359731,-1.08333333333333));
#41715=CARTESIAN_POINT('Ctrl Pts',(13.0926472341269,-7.16598374096113,-1.08333333333333));
#41716=CARTESIAN_POINT('Ctrl Pts',(12.8106483205942,-7.10161932916216,-1.08333333333333));
#41717=CARTESIAN_POINT('Ctrl Pts',(12.6155690741987,-7.02043310055321,-1.08333333333333));
#41718=CARTESIAN_POINT('Ctrl Pts',(12.4579905368414,-6.91816245718254,-1.08333333333333));
#41719=CARTESIAN_POINT('',(12.4579905368491,-6.91816245718746,1.08333333333334));
#41720=CARTESIAN_POINT('Ctrl Pts',(12.4579905368414,-6.91816245718254,1.08333333333318));
#41721=CARTESIAN_POINT('Ctrl Pts',(12.4412857888865,-6.94824379644432,0.949270311030419));
#41722=CARTESIAN_POINT('Ctrl Pts',(12.4276027080704,-6.97263587945666,0.813521288368017));
#41723=CARTESIAN_POINT('Ctrl Pts',(12.4170780656486,-6.99132836531005,0.676607052101155));
#41724=CARTESIAN_POINT('Ctrl Pts',(12.4080806643215,-7.00730836636693,0.559560573777918));
#41725=CARTESIAN_POINT('Ctrl Pts',(12.4013908554088,-7.019122574986,0.441662516279092));
#41726=CARTESIAN_POINT('Ctrl Pts',(12.397067491958,-7.0267501449702,0.323238258334718));
#41727=CARTESIAN_POINT('Ctrl Pts',(12.3920718206831,-7.03556384585387,0.186398348762654));
#41728=CARTESIAN_POINT('Ctrl Pts',(12.3902516338787,-7.03876210460539,0.0492519096262223));
#41729=CARTESIAN_POINT('Ctrl Pts',(12.3916053560035,-7.03637809537437,-0.0876758270660355));
#41730=CARTESIAN_POINT('Ctrl Pts',(12.3929630026023,-7.03398717484161,-0.225000520654302));
#41731=CARTESIAN_POINT('Ctrl Pts',(12.3975129673672,-7.02598155019911,-0.362105241912753));
#41732=CARTESIAN_POINT('Ctrl Pts',(12.4052079364272,-7.01236879050172,-0.498460177595601));
#41733=CARTESIAN_POINT('Ctrl Pts',(12.4129361026925,-6.99869730339771,-0.635403368116608));
#41734=CARTESIAN_POINT('Ctrl Pts',(12.4238364813948,-6.9793701376568,-0.771590289741124));
#41735=CARTESIAN_POINT('Ctrl Pts',(12.4378151222668,-6.95436948862457,-0.906484242526394));
#41736=CARTESIAN_POINT('Ctrl Pts',(12.4439512822523,-6.94339503240884,-0.96569821639967));
#41737=CARTESIAN_POINT('Ctrl Pts',(12.4506800022041,-6.93132701813272,-1.0246630456538));
#41738=CARTESIAN_POINT('Ctrl Pts',(12.4579905368414,-6.91816245718254,-1.08333333333318));
#41739=CARTESIAN_POINT('',(13.3303603014235,-7.18268588222768,1.08333333333334));
#41740=CARTESIAN_POINT('Ctrl Pts',(13.3303603014235,-7.18268588222769,1.08333333333333));
#41741=CARTESIAN_POINT('Ctrl Pts',(13.2116326209361,-7.18117853359731,1.08333333333333));
#41742=CARTESIAN_POINT('Ctrl Pts',(13.0926472341269,-7.16598374096113,1.08333333333333));
#41743=CARTESIAN_POINT('Ctrl Pts',(12.810648320597,-7.10161932916281,1.08333333333333));
#41744=CARTESIAN_POINT('Ctrl Pts',(12.6155690742049,-7.020433100556,1.08333333333333));
#41745=CARTESIAN_POINT('Ctrl Pts',(12.4579905368491,-6.91816245718749,1.08333333333333));
#41746=CARTESIAN_POINT('Ctrl Pts',(13.3303603014235,-7.18268588222769,-1.08333333333333));
#41747=CARTESIAN_POINT('Ctrl Pts',(13.3126024326051,-7.21564274452345,-0.956888632103319));
#41748=CARTESIAN_POINT('Ctrl Pts',(13.2978764135175,-7.24268913148574,-0.828820583351199));
#41749=CARTESIAN_POINT('Ctrl Pts',(13.2863164700112,-7.26383348564869,-0.699646919261793));
#41750=CARTESIAN_POINT('Ctrl Pts',(13.2748173090023,-7.28486666222208,-0.57115245381317));
#41751=CARTESIAN_POINT('Ctrl Pts',(13.2664510227834,-7.30005980724128,-0.441563969171537));
#41752=CARTESIAN_POINT('Ctrl Pts',(13.2613042752927,-7.30939745578421,-0.311391073637702));
#41753=CARTESIAN_POINT('Ctrl Pts',(13.2561988309336,-7.31866016882124,-0.182262827807302));
#41754=CARTESIAN_POINT('Ctrl Pts',(13.2542614634095,-7.32216103446727,-0.0525595133519065));
#41755=CARTESIAN_POINT('Ctrl Pts',(13.2555318677529,-7.3198604598385,0.0772214321948015));
#41756=CARTESIAN_POINT('Ctrl Pts',(13.2563983335702,-7.31829137729713,0.16573715053459));
#41757=CARTESIAN_POINT('Ctrl Pts',(13.2587560588235,-7.31402308269219,0.254288981130321));
#41758=CARTESIAN_POINT('Ctrl Pts',(13.2626054360147,-7.30703628683439,0.342719102199534));
#41759=CARTESIAN_POINT('Ctrl Pts',(13.2684086950193,-7.29650310602066,0.476034927301568));
#41760=CARTESIAN_POINT('Ctrl Pts',(13.2775701666805,-7.2798543418706,0.608312350205377));
#41761=CARTESIAN_POINT('Ctrl Pts',(13.289943417625,-7.25719547792716,0.739057191237071));
#41762=CARTESIAN_POINT('Ctrl Pts',(13.300929037023,-7.23707775329776,0.8551392999939));
#41763=CARTESIAN_POINT('Ctrl Pts',(13.3144456587152,-7.21222189770271,0.970013302477615));
#41764=CARTESIAN_POINT('Ctrl Pts',(13.3303603014235,-7.18268588222769,1.08333333333334));
#41765=CARTESIAN_POINT('Origin',(13.892722748591,-3.17092330887735,3.20017169526122E-15));
#41766=CARTESIAN_POINT('',(15.1423033840733,-0.0114224867026808,1.08333333333334));
#41767=CARTESIAN_POINT('',(14.6487667980729,0.141522102769127,1.08333333333334));
#41768=CARTESIAN_POINT('Origin',(13.892722748591,-3.17092330887735,1.08333333333334));
#41769=CARTESIAN_POINT('',(15.1423033840733,-0.0114224867026808,-1.08333333333333));
#41770=CARTESIAN_POINT('Ctrl Pts',(15.1423033840733,-0.0114224867026917,
-1.08333333333333));
#41771=CARTESIAN_POINT('Ctrl Pts',(15.1423953499066,0.110492695607724,-0.727666221822789));
#41772=CARTESIAN_POINT('Ctrl Pts',(15.1413590080604,0.169498193350193,-0.352782973842772));
#41773=CARTESIAN_POINT('Ctrl Pts',(15.1413590080604,0.169498193350193,0.352782973842778));
#41774=CARTESIAN_POINT('Ctrl Pts',(15.1423953499066,0.110492695607724,0.727666221822797));
#41775=CARTESIAN_POINT('Ctrl Pts',(15.1423033840733,-0.0114224867026924,
1.08333333333334));
#41776=CARTESIAN_POINT('',(14.2484814298548,0.208031110850763,-1.08333333333333));
#41777=CARTESIAN_POINT('Origin',(13.892722748591,-3.17092330887735,-1.08333333333333));
#41778=CARTESIAN_POINT('',(14.2484814298548,0.208031110850763,1.08333333333334));
#41779=CARTESIAN_POINT('Ctrl Pts',(14.2484814298548,0.208031110850764,1.08333333333334));
#41780=CARTESIAN_POINT('Ctrl Pts',(14.2468058395578,0.322795758952199,0.725928647976585));
#41781=CARTESIAN_POINT('Ctrl Pts',(14.2449910310593,0.377796936249431,0.352039859176993));
#41782=CARTESIAN_POINT('Ctrl Pts',(14.2449910310593,0.37779693624943,-0.352039859176987));
#41783=CARTESIAN_POINT('Ctrl Pts',(14.2468058395578,0.322795758952199,-0.725928647976577));
#41784=CARTESIAN_POINT('Ctrl Pts',(14.2484814298548,0.208031110850765,-1.08333333333333));
#41785=CARTESIAN_POINT('Origin',(13.892722748591,-3.17092330887735,1.08333333333334));
#41786=CARTESIAN_POINT('',(13.1366786991091,-6.48336872052383,1.08333333333334));
#41787=CARTESIAN_POINT('Origin',(13.892722748591,-3.17092330887735,3.20017169526122E-15));
#41788=CARTESIAN_POINT('',(12.7471768669564,-6.36961395396396,1.08333333333334));
#41789=CARTESIAN_POINT('Origin',(13.892722748591,-3.17092330887735,1.08333333333334));
#41790=CARTESIAN_POINT('',(12.7471768669564,-6.36961395396396,-1.08333333333333));
#41791=CARTESIAN_POINT('Ctrl Pts',(12.7471768669564,-6.36961395396397,-1.08333333333334));
#41792=CARTESIAN_POINT('Ctrl Pts',(12.6958726976266,-6.47228631765585,-0.725928647976583));
#41793=CARTESIAN_POINT('Ctrl Pts',(12.6703734952067,-6.52105325020152,-0.352039859176989));
#41794=CARTESIAN_POINT('Ctrl Pts',(12.6703734952067,-6.52105325020152,3.73360976135914E-15));
#41795=CARTESIAN_POINT('Ctrl Pts',(12.6703734952067,-6.52105325020152,0.352039859176996));
#41796=CARTESIAN_POINT('Ctrl Pts',(12.6958726976266,-6.47228631765585,0.725928647976591));
#41797=CARTESIAN_POINT('Ctrl Pts',(12.7471768669564,-6.36961395396397,1.08333333333335));
#41798=CARTESIAN_POINT('',(13.6476999686242,-6.55970790622078,-1.08333333333333));
#41799=CARTESIAN_POINT('Origin',(13.892722748591,-3.17092330887735,-1.08333333333333));
#41800=CARTESIAN_POINT('',(13.6476999686242,-6.55970790622078,1.08333333333334));
#41801=CARTESIAN_POINT('Ctrl Pts',(13.6476999686242,-6.55970790622078,1.08333333333334));
#41802=CARTESIAN_POINT('Ctrl Pts',(13.5948858118209,-6.66958959248674,0.727666221822799));
#41803=CARTESIAN_POINT('Ctrl Pts',(13.5683505740919,-6.72230205711255,0.35278297384278));
#41804=CARTESIAN_POINT('Ctrl Pts',(13.5683505740919,-6.72230205711255,3.93962482987281E-15));
#41805=CARTESIAN_POINT('Ctrl Pts',(13.5683505740919,-6.72230205711255,-0.352782973842771));
#41806=CARTESIAN_POINT('Ctrl Pts',(13.5948858118209,-6.66958959248674,-0.72766622182279));
#41807=CARTESIAN_POINT('Ctrl Pts',(13.6476999686242,-6.55970790622078,-1.08333333333333));
#41808=CARTESIAN_POINT('Origin',(13.892722748591,-3.17092330887735,1.08333333333334));
#41809=CARTESIAN_POINT('',(13.0227870731057,-2.97236616780865,-3.45272288248773));
#41810=CARTESIAN_POINT('Origin',(13.0227870731057,-2.97236616780865,2.9997830762867E-15));
#41811=CARTESIAN_POINT('',(14.7626584240763,-3.36948044994605,-3.45272288248773));
#41812=CARTESIAN_POINT('Origin',(14.7626584240763,-3.36948044994605,3.40056031423575E-15));
#41813=CARTESIAN_POINT('Origin',(11.1410986251693,8.88472967648709,9.85584169237555E-16));
#41814=CARTESIAN_POINT('',(11.8387328710639,9.44107442276104,3.96060240207311));
#41815=CARTESIAN_POINT('Origin',(11.8387328710639,9.44107442276104,1.0472995612114E-15));
#41816=CARTESIAN_POINT('',(10.4434643792748,8.32838493021314,3.96060240207311));
#41817=CARTESIAN_POINT('Origin',(11.1410986251693,8.88472967648709,2.5198520116158));
#41818=CARTESIAN_POINT('Origin',(10.4434643792748,8.32838493021314,9.23868777263706E-16));
#41819=CARTESIAN_POINT('',(8.89378902201275,12.2552029391784,-1.08333333331655));
#41820=CARTESIAN_POINT('',(8.89378902201677,12.2552029391754,1.08333333333333));
#41821=CARTESIAN_POINT('Ctrl Pts',(8.89378902201274,12.2552029391784,-1.08333333331655));
#41822=CARTESIAN_POINT('Ctrl Pts',(8.86335293025879,12.2772908784853,-0.956315399884826));
#41823=CARTESIAN_POINT('Ctrl Pts',(8.83824313040494,12.2953456493747,-0.827586922367285));
#41824=CARTESIAN_POINT('Ctrl Pts',(8.81859777764014,12.3094197866805,-0.69766772380084));
#41825=CARTESIAN_POINT('Ctrl Pts',(8.7991879276401,12.3233252073292,-0.569305958731489));
#41826=CARTESIAN_POINT('Ctrl Pts',(8.78511225071473,12.3333449381983,-0.439781849534452));
#41827=CARTESIAN_POINT('Ctrl Pts',(8.77647376760361,12.3394890678296,-0.309596747993595));
#41828=CARTESIAN_POINT('Ctrl Pts',(8.76964787761092,12.344343988818,-0.206728088024587));
#41829=CARTESIAN_POINT('Ctrl Pts',(8.76621624622163,12.3467783236357,-0.103446722778746));
#41830=CARTESIAN_POINT('Ctrl Pts',(8.76621624622163,12.3467783236357,-7.54951656745106E-15));
#41831=CARTESIAN_POINT('Ctrl Pts',(8.76621624622163,12.3467783236357,0.130951008152141));
#41832=CARTESIAN_POINT('Ctrl Pts',(8.77171477448527,12.3428797767713,0.261548325668487));
#41833=CARTESIAN_POINT('Ctrl Pts',(8.78261416841303,12.3351194002049,0.391301356121213));
#41834=CARTESIAN_POINT('Ctrl Pts',(8.79368558213778,12.3272365454154,0.523102215114213));
#41835=CARTESIAN_POINT('Ctrl Pts',(8.81032969837903,12.3153689336875,0.654031926803563));
#41836=CARTESIAN_POINT('Ctrl Pts',(8.83241243050519,12.2995110840219,0.783576297698762));
#41837=CARTESIAN_POINT('Ctrl Pts',(8.84960195907419,12.2871670969504,0.88441557119687));
#41838=CARTESIAN_POINT('Ctrl Pts',(8.87008627043973,12.2724043900869,0.984415425401903));
#41839=CARTESIAN_POINT('Ctrl Pts',(8.89378902201675,12.2552029391755,1.08333333333333));
#41840=CARTESIAN_POINT('',(8.22258343557123,11.6383685130292,1.08333333333333));
#41841=CARTESIAN_POINT('Ctrl Pts',(8.89378902201675,12.2552029391755,1.08333333333333));
#41842=CARTESIAN_POINT('Ctrl Pts',(8.78751907456219,12.2023537225759,1.08333333333333));
#41843=CARTESIAN_POINT('Ctrl Pts',(8.68681488082489,12.1369760343758,1.08333333333333));
#41844=CARTESIAN_POINT('Ctrl Pts',(8.46069343470621,11.9566501984405,1.08333333333333));
#41845=CARTESIAN_POINT('Ctrl Pts',(8.31988542322917,11.7983921800676,1.08333333333333));
#41846=CARTESIAN_POINT('Ctrl Pts',(8.22258343557176,11.6383685130289,1.08333333333333));
#41847=CARTESIAN_POINT('',(8.22258343557175,11.6383685130288,-1.08333333333333));
#41848=CARTESIAN_POINT('Ctrl Pts',(8.2225834355717,11.6383685130289,1.08333333333318));
#41849=CARTESIAN_POINT('Ctrl Pts',(8.19448780675769,11.6582182584498,0.949301954017324));
#41850=CARTESIAN_POINT('Ctrl Pts',(8.17159767874311,11.6742430454627,0.81366496302888));
#41851=CARTESIAN_POINT('Ctrl Pts',(8.15402161030241,11.6865063889394,0.67695567866062));
#41852=CARTESIAN_POINT('Ctrl Pts',(8.13658119548769,11.6986750828637,0.541301528447691));
#41853=CARTESIAN_POINT('Ctrl Pts',(8.12437307855494,11.7071402381473,0.40459157308691));
#41854=CARTESIAN_POINT('Ctrl Pts',(8.1174733585697,11.7119223986889,0.26734687734235));
#41855=CARTESIAN_POINT('Ctrl Pts',(8.11300215046573,11.7150213700985,0.178408544025479));
#41856=CARTESIAN_POINT('Ctrl Pts',(8.11075954642938,11.7165728598428,0.0892456520429063));
#41857=CARTESIAN_POINT('Ctrl Pts',(8.11075954642938,11.7165728598428,-1.33226762955019E-15));
#41858=CARTESIAN_POINT('Ctrl Pts',(8.11075954642938,11.7165728598428,-0.137335411050026));
#41859=CARTESIAN_POINT('Ctrl Pts',(8.11607262981309,11.7129002012938,-0.274553571737022));
#41860=CARTESIAN_POINT('Ctrl Pts',(8.12665801674411,11.7055512249056,-0.411127959090392));
#41861=CARTESIAN_POINT('Ctrl Pts',(8.13729388250879,11.698167203246,-0.548353632582512));
#41862=CARTESIAN_POINT('Ctrl Pts',(8.15325248641432,11.6870716767896,-0.684929378140945));
#41863=CARTESIAN_POINT('Ctrl Pts',(8.17446212457132,11.6722178258439,-0.820321104282498));
#41864=CARTESIAN_POINT('Ctrl Pts',(8.18828255682692,11.6625388940673,-0.908543834215877));
#41865=CARTESIAN_POINT('Ctrl Pts',(8.20433194575505,11.6512633098961,-0.9962638332735));
#41866=CARTESIAN_POINT('Ctrl Pts',(8.22258343557176,11.6383685130288,-1.08333333333334));
#41867=CARTESIAN_POINT('Ctrl Pts',(8.89378902201473,12.2552029391744,-1.08333333333333));
#41868=CARTESIAN_POINT('Ctrl Pts',(8.7875190745609,12.202353722575,-1.08333333333333));
#41869=CARTESIAN_POINT('Ctrl Pts',(8.68681488082435,12.1369760343753,-1.08333333333333));
#41870=CARTESIAN_POINT('Ctrl Pts',(8.46069343470619,11.9566501984405,-1.08333333333333));
#41871=CARTESIAN_POINT('Ctrl Pts',(8.31988542322913,11.7983921800676,-1.08333333333333));
#41872=CARTESIAN_POINT('Ctrl Pts',(8.22258343557172,11.6383685130288,-1.08333333333333));
#41873=CARTESIAN_POINT('',(13.9269936544443,5.94376395877129,-1.08333333333333));
#41874=CARTESIAN_POINT('',(13.1762672612271,5.42664547033562,-1.08333333333333));
#41875=CARTESIAN_POINT('Ctrl Pts',(13.9269936544443,5.94376395877129,-1.08333333333333));
#41876=CARTESIAN_POINT('Ctrl Pts',(13.8517896638478,5.85187873682469,-1.08333333333333));
#41877=CARTESIAN_POINT('Ctrl Pts',(13.7657237213495,5.76832601371371,-1.08333333333333));
#41878=CARTESIAN_POINT('Ctrl Pts',(13.5395781511316,5.5879809394513,-1.08333333333333));
#41879=CARTESIAN_POINT('Ctrl Pts',(13.3544742809805,5.48608062863226,-1.08333333333333));
#41880=CARTESIAN_POINT('Ctrl Pts',(13.1762672612269,5.42664547033621,-1.08333333333333));
#41881=CARTESIAN_POINT('',(13.1762672612355,5.42664547033908,1.08333333333333));
#41882=CARTESIAN_POINT('Ctrl Pts',(13.1762672612269,5.42664547033617,1.08333333333318));
#41883=CARTESIAN_POINT('Ctrl Pts',(13.1893705593041,5.39482976422236,0.949270311030452));
#41884=CARTESIAN_POINT('Ctrl Pts',(13.1999097963792,5.36892368585892,0.813521288368082));
#41885=CARTESIAN_POINT('Ctrl Pts',(13.2079621630868,5.34904061477083,0.676607052101254));
#41886=CARTESIAN_POINT('Ctrl Pts',(13.2148460430323,5.33204279546023,0.559560573777983));
#41887=CARTESIAN_POINT('Ctrl Pts',(13.2199117356377,5.31944645364959,0.441662516279123));
#41888=CARTESIAN_POINT('Ctrl Pts',(13.2231796369647,5.31131059989547,0.323238258334714));
#41889=CARTESIAN_POINT('Ctrl Pts',(13.2269557156993,5.30190957419912,0.186398348762647));
#41890=CARTESIAN_POINT('Ctrl Pts',(13.2283213471703,5.2984924131362,0.0492519096262126));
#41891=CARTESIAN_POINT('Ctrl Pts',(13.2273014856384,5.30103720115497,-0.087675827066048));
#41892=CARTESIAN_POINT('Ctrl Pts',(13.2262786675026,5.30358936657715,-0.225000520654307));
#41893=CARTESIAN_POINT('Ctrl Pts',(13.22285647475,5.31213809759657,-0.362105241912749));
#41894=CARTESIAN_POINT('Ctrl Pts',(13.2170113253899,5.32664168351083,-0.498460177595588));
#41895=CARTESIAN_POINT('Ctrl Pts',(13.2111409592133,5.34120783998435,-0.635403368116607));
#41896=CARTESIAN_POINT('Ctrl Pts',(13.2028266475275,5.36178038996296,-0.771590289741134));
#41897=CARTESIAN_POINT('Ctrl Pts',(13.1919958930594,5.38829698119018,-0.906484242526414));
#41898=CARTESIAN_POINT('Ctrl Pts',(13.1872415508606,5.3999368857798,-0.965698216399684));
#41899=CARTESIAN_POINT('Ctrl Pts',(13.1820016856381,5.41272189470467,-1.02466304565381));
#41900=CARTESIAN_POINT('Ctrl Pts',(13.1762672612269,5.42664547033617,-1.08333333333318));
#41901=CARTESIAN_POINT('',(13.9269936544443,5.94376395877129,1.08333333333333));
#41902=CARTESIAN_POINT('Ctrl Pts',(13.9269936544443,5.94376395877129,1.08333333333333));
#41903=CARTESIAN_POINT('Ctrl Pts',(13.8517896638478,5.85187873682469,1.08333333333333));
#41904=CARTESIAN_POINT('Ctrl Pts',(13.7657237213495,5.76832601371371,1.08333333333333));
#41905=CARTESIAN_POINT('Ctrl Pts',(13.5395781511339,5.5879809394531,1.08333333333333));
#41906=CARTESIAN_POINT('Ctrl Pts',(13.3544742809865,5.48608062863536,1.08333333333333));
#41907=CARTESIAN_POINT('Ctrl Pts',(13.1762672612355,5.42664547033908,1.08333333333333));
#41908=CARTESIAN_POINT('Ctrl Pts',(13.9269936544443,5.9437639587713,-1.08333333333333));
#41909=CARTESIAN_POINT('Ctrl Pts',(13.9416885168395,5.90933203032488,-0.95688863210334));
#41910=CARTESIAN_POINT('Ctrl Pts',(13.9536527109305,5.88095561854266,-0.828820583351241));
#41911=CARTESIAN_POINT('Ctrl Pts',(13.9629765258053,5.85873440158633,-0.699646919261855));
#41912=CARTESIAN_POINT('Ctrl Pts',(13.9722513158077,5.83663002439342,-0.571152453813261));
#41913=CARTESIAN_POINT('Ctrl Pts',(13.9789135007645,5.82061622745854,-0.441563969171658));
#41914=CARTESIAN_POINT('Ctrl Pts',(13.9830050237944,5.81077040959811,-0.31139107363785));
#41915=CARTESIAN_POINT('Ctrl Pts',(13.987063711968,5.80100360535004,-0.182262827807452));
#41916=CARTESIAN_POINT('Ctrl Pts',(13.9885928700522,5.79730615639857,-0.0525595133520559));
#41917=CARTESIAN_POINT('Ctrl Pts',(13.9875862925321,5.79973378332923,0.077221432194654));
#41918=CARTESIAN_POINT('Ctrl Pts',(13.9868997670033,5.80138952054645,0.165737150534494));
#41919=CARTESIAN_POINT('Ctrl Pts',(13.9850326975557,5.80589410253397,0.254288981130278));
#41920=CARTESIAN_POINT('Ctrl Pts',(13.9819702480148,5.81325986277498,0.342719102199545));
#41921=CARTESIAN_POINT('Ctrl Pts',(13.977353348451,5.82436436418423,0.476034927301432));
#41922=CARTESIAN_POINT('Ctrl Pts',(13.9700489046451,5.84190742581571,0.608312350205104));
#41923=CARTESIAN_POINT('Ctrl Pts',(13.9600480872369,5.86570879353505,0.739057191236667));
#41924=CARTESIAN_POINT('Ctrl Pts',(13.9511688384277,5.88684089277784,0.855139299993628));
#41925=CARTESIAN_POINT('Ctrl Pts',(13.9401632237805,5.91290598563348,0.970013302477476));
#41926=CARTESIAN_POINT('Ctrl Pts',(13.9269936544443,5.9437639587713,1.08333333333333));
#41927=CARTESIAN_POINT('Origin',(11.1410986251693,8.88472967648709,9.85584169237555E-16));
#41928=CARTESIAN_POINT('',(8.72113759169208,11.2696166353064,1.08333333333333));
#41929=CARTESIAN_POINT('',(9.02271027299523,11.54110464988,1.08333333333333));
#41930=CARTESIAN_POINT('Origin',(11.1410986251693,8.88472967648709,1.08333333333333));
#41931=CARTESIAN_POINT('',(13.2594869773434,6.22835470309422,1.08333333333333));
#41932=CARTESIAN_POINT('Origin',(11.1410986251693,8.88472967648709,9.85584169237555E-16));
#41933=CARTESIAN_POINT('',(12.9276994994135,5.9947548451011,1.08333333333333));
#41934=CARTESIAN_POINT('Origin',(11.1410986251693,8.88472967648709,1.08333333333333));
#41935=CARTESIAN_POINT('',(12.9276994994135,5.9947548451011,-1.08333333333333));
#41936=CARTESIAN_POINT('Ctrl Pts',(12.9276994994135,5.9947548451011,-1.08333333333333));
#41937=CARTESIAN_POINT('Ctrl Pts',(12.9759843593573,5.89062845864264,-0.725928647976581));
#41938=CARTESIAN_POINT('Ctrl Pts',(12.9982133898606,5.84028669430273,-0.352039859176989));
#41939=CARTESIAN_POINT('Ctrl Pts',(12.9982133898606,5.84028669430273,9.85141416048961E-16));
#41940=CARTESIAN_POINT('Ctrl Pts',(12.9982133898606,5.84028669430273,0.35203985917699));
#41941=CARTESIAN_POINT('Ctrl Pts',(12.9759843593573,5.89062845864264,0.72592864797658));
#41942=CARTESIAN_POINT('Ctrl Pts',(12.9276994994135,5.9947548451011,1.08333333333333));
#41943=CARTESIAN_POINT('',(13.6377879061428,6.58029051604763,-1.08333333333333));
#41944=CARTESIAN_POINT('Origin',(11.1410986251693,8.88472967648709,-1.08333333333333));
#41945=CARTESIAN_POINT('',(13.6377879061428,6.58029051604763,1.08333333333333));
#41946=CARTESIAN_POINT('Ctrl Pts',(13.6377879061428,6.58029051604764,1.08333333333332));
#41947=CARTESIAN_POINT('Ctrl Pts',(13.6907677796515,6.47048863474093,0.727666221822788));
#41948=CARTESIAN_POINT('Ctrl Pts',(13.7154355939006,6.41687686636464,0.352782973842773));
#41949=CARTESIAN_POINT('Ctrl Pts',(13.7154355939006,6.41687686636464,9.86054494281319E-16));
#41950=CARTESIAN_POINT('Ctrl Pts',(13.7154355939006,6.41687686636464,-0.352782973842772));
#41951=CARTESIAN_POINT('Ctrl Pts',(13.6907677796515,6.47048863474094,-0.727666221822788));
#41952=CARTESIAN_POINT('Ctrl Pts',(13.6377879061428,6.58029051604764,-1.08333333333332));
#41953=CARTESIAN_POINT('Origin',(11.1410986251693,8.88472967648709,1.08333333333333));
#41954=CARTESIAN_POINT('',(9.4500021963329,11.8316076987797,1.08333333333333));
#41955=CARTESIAN_POINT('Origin',(11.1410986251693,8.88472967648709,1.08333333333333));
#41956=CARTESIAN_POINT('',(9.4500021963329,11.8316076987797,-1.08333333333333));
#41957=CARTESIAN_POINT('Ctrl Pts',(9.4500021963329,11.8316076987798,1.08333333333334));
#41958=CARTESIAN_POINT('Ctrl Pts',(9.35474240837097,11.9076924734258,0.7276662218228));
#41959=CARTESIAN_POINT('Ctrl Pts',(9.30796390402485,11.9436715548399,0.352782973842779));
#41960=CARTESIAN_POINT('Ctrl Pts',(9.30796390402485,11.9436715548399,-0.352782973842777));
#41961=CARTESIAN_POINT('Ctrl Pts',(9.35474240837097,11.9076924734258,-0.7276662218228));
#41962=CARTESIAN_POINT('Ctrl Pts',(9.4500021963329,11.8316076987798,-1.08333333333334));
#41963=CARTESIAN_POINT('',(8.72113759169208,11.2696166353064,-1.08333333333333));
#41964=CARTESIAN_POINT('Origin',(11.1410986251693,8.88472967648709,-1.08333333333333));
#41965=CARTESIAN_POINT('Ctrl Pts',(8.72113759169207,11.2696166353064,-1.08333333333334));
#41966=CARTESIAN_POINT('Ctrl Pts',(8.63036626326973,11.3398611937657,-0.725928647976583));
#41967=CARTESIAN_POINT('Ctrl Pts',(8.5862330966948,11.3727349924819,-0.35203985917699));
#41968=CARTESIAN_POINT('Ctrl Pts',(8.5862330966948,11.3727349924819,0.352039859176991));
#41969=CARTESIAN_POINT('Ctrl Pts',(8.63036626326973,11.3398611937657,0.725928647976584));
#41970=CARTESIAN_POINT('Ctrl Pts',(8.72113759169207,11.2696166353064,1.08333333333334));
#41971=CARTESIAN_POINT('',(10.4434643792748,8.32838493021314,-3.45272288248773));
#41972=CARTESIAN_POINT('Origin',(10.4434643792748,8.32838493021314,9.23868777263706E-16));
#41973=CARTESIAN_POINT('',(11.8387328710639,9.44107442276105,-3.45272288248773));
#41974=CARTESIAN_POINT('Origin',(11.8387328710639,9.44107442276104,1.0472995612114E-15));
#41975=CARTESIAN_POINT('Origin',(0.,14.25,0.));
#41976=CARTESIAN_POINT('',(-3.35834339016074,14.7651959662676,1.08333333333333));
#41977=CARTESIAN_POINT('',(-3.39763111739558,14.25,1.08333333333333));
#41978=CARTESIAN_POINT('Origin',(1.55588456152529E-16,14.25,1.08333333333333));
#41979=CARTESIAN_POINT('',(-3.35834339016074,14.7651959662676,-1.08333333333333));
#41980=CARTESIAN_POINT('Ctrl Pts',(-3.35834339016074,14.7651959662676,-1.08333333333333));
#41981=CARTESIAN_POINT('Ctrl Pts',(-3.47722236863702,14.7381569460943,-0.727666221822795));
#41982=CARTESIAN_POINT('Ctrl Pts',(-3.53451786760282,14.7240166290356,-0.352782973842776));
#41983=CARTESIAN_POINT('Ctrl Pts',(-3.53451786760282,14.7240166290356,0.352782973842775));
#41984=CARTESIAN_POINT('Ctrl Pts',(-3.47722236863702,14.7381569460943,0.727666221822794));
#41985=CARTESIAN_POINT('Ctrl Pts',(-3.35834339016074,14.7651959662676,1.08333333333333));
#41986=CARTESIAN_POINT('',(-3.37340073180097,13.8449509750914,-1.08333333333333));
#41987=CARTESIAN_POINT('Origin',(-1.5558845615253E-16,14.25,-1.08333333333333));
#41988=CARTESIAN_POINT('',(-3.37340073180097,13.8449509750914,1.08333333333333));
#41989=CARTESIAN_POINT('Ctrl Pts',(-3.37340073180098,13.8449509750914,1.08333333333333));
#41990=CARTESIAN_POINT('Ctrl Pts',(-3.48491513664897,13.8177798586608,0.725928647976578));
#41991=CARTESIAN_POINT('Ctrl Pts',(-3.53813348671686,13.8037716378594,0.352039859176988));
#41992=CARTESIAN_POINT('Ctrl Pts',(-3.53813348671686,13.8037716378594,-0.352039859176988));
#41993=CARTESIAN_POINT('Ctrl Pts',(-3.48491513664897,13.8177798586608,-0.725928647976578));
#41994=CARTESIAN_POINT('Ctrl Pts',(-3.37340073180098,13.8449509750914,-1.08333333333333));
#41995=CARTESIAN_POINT('Origin',(1.55588456152529E-16,14.25,1.08333333333333));
#41996=CARTESIAN_POINT('',(3.39763111739558,14.25,1.08333333333333));
#41997=CARTESIAN_POINT('Origin',(0.,14.25,0.));
#41998=CARTESIAN_POINT('',(3.37340073180097,13.8449509750914,1.08333333333333));
#41999=CARTESIAN_POINT('Origin',(0.,14.25,1.08333333333333));
#42000=CARTESIAN_POINT('',(3.37340073180097,13.8449509750914,-1.08333333333333));
#42001=CARTESIAN_POINT('Ctrl Pts',(3.37340073180098,13.8449509750914,-1.08333333333333));
#42002=CARTESIAN_POINT('Ctrl Pts',(3.48491513664897,13.8177798586608,-0.725928647976578));
#42003=CARTESIAN_POINT('Ctrl Pts',(3.53813348671686,13.8037716378594,-0.352039859176988));
#42004=CARTESIAN_POINT('Ctrl Pts',(3.53813348671686,13.8037716378594,0.));
#42005=CARTESIAN_POINT('Ctrl Pts',(3.53813348671686,13.8037716378594,0.352039859176988));
#42006=CARTESIAN_POINT('Ctrl Pts',(3.48491513664897,13.8177798586608,0.725928647976578));
#42007=CARTESIAN_POINT('Ctrl Pts',(3.37340073180098,13.8449509750914,1.08333333333333));
#42008=CARTESIAN_POINT('',(3.35834339016074,14.7651959662676,-1.08333333333333));
#42009=CARTESIAN_POINT('Origin',(0.,14.25,-1.08333333333333));
#42010=CARTESIAN_POINT('',(3.35834339016074,14.7651959662676,1.08333333333333));
#42011=CARTESIAN_POINT('Ctrl Pts',(3.35834339016074,14.7651959662676,1.08333333333333));
#42012=CARTESIAN_POINT('Ctrl Pts',(3.47722236863702,14.7381569460943,0.727666221822794));
#42013=CARTESIAN_POINT('Ctrl Pts',(3.53451786760282,14.7240166290356,0.352782973842775));
#42014=CARTESIAN_POINT('Ctrl Pts',(3.53451786760282,14.7240166290356,0.));
#42015=CARTESIAN_POINT('Ctrl Pts',(3.53451786760282,14.7240166290356,-0.352782973842775));
#42016=CARTESIAN_POINT('Ctrl Pts',(3.47722236863702,14.7381569460943,-0.727666221822793));
#42017=CARTESIAN_POINT('Ctrl Pts',(3.35834339016074,14.7651959662676,-1.08333333333333));
#42018=CARTESIAN_POINT('Origin',(0.,14.25,1.08333333333333));
#42019=CARTESIAN_POINT('',(0.,13.3576923076923,-3.45272288248773));
#42020=CARTESIAN_POINT('Origin',(0.,13.3576923076923,0.));
#42021=CARTESIAN_POINT('',(0.,15.1423076923077,-3.45272288248773));
#42022=CARTESIAN_POINT('Origin',(0.,15.1423076923077,0.));
#42023=CARTESIAN_POINT('Origin',(0.,14.25,0.));
#42024=CARTESIAN_POINT('',(-4.85033905439415E-16,15.1423076923077,3.96060240207311));
#42025=CARTESIAN_POINT('Origin',(0.,15.1423076923077,0.));
#42026=CARTESIAN_POINT('',(-4.85033905439415E-16,13.3576923076923,3.96060240207311));
#42027=CARTESIAN_POINT('Origin',(3.08592870035031E-16,14.25,2.5198520116158));
#42028=CARTESIAN_POINT('Origin',(0.,13.3576923076923,0.));
#42029=CARTESIAN_POINT('',(-3.97254599103887,13.6850786752975,-1.08333333333333));
#42030=CARTESIAN_POINT('',(-4.03631672677061,14.5944383081266,-1.08333333333333));
#42031=CARTESIAN_POINT('Ctrl Pts',(-3.97254599103889,13.6850786752975,-1.08333333333333));
#42032=CARTESIAN_POINT('Ctrl Pts',(-4.03699073486477,13.8609255570095,-1.08333333333333));
#42033=CARTESIAN_POINT('Ctrl Pts',(-4.07292947680577,14.0696859538838,-1.08333333333333));
#42034=CARTESIAN_POINT('Ctrl Pts',(-4.07292947680577,14.358906139038,-1.08333333333333));
#42035=CARTESIAN_POINT('Ctrl Pts',(-4.06125577389194,14.4784021699804,-1.08333333333333));
#42036=CARTESIAN_POINT('Ctrl Pts',(-4.03631672677123,14.5944383081267,-1.08333333333333));
#42037=CARTESIAN_POINT('',(-4.03631672677098,14.5944383081279,1.08333333333333));
#42038=CARTESIAN_POINT('Ctrl Pts',(-4.03631672677125,14.5944383081264,1.08333333333353));
#42039=CARTESIAN_POINT('Ctrl Pts',(-4.07239878927587,14.5844592579328,0.956888632103535));
#42040=CARTESIAN_POINT('Ctrl Pts',(-4.10204391436992,14.576120838176,0.828820583351431));
#42041=CARTESIAN_POINT('Ctrl Pts',(-4.12523046485396,14.5695557880246,0.699646919262042));
#42042=CARTESIAN_POINT('Ctrl Pts',(-4.14829509982461,14.5630252570856,0.571152453813459));
#42043=CARTESIAN_POINT('Ctrl Pts',(-4.16496899480084,14.5582495239489,0.441563969171867));
#42044=CARTESIAN_POINT('Ctrl Pts',(-4.17521778805797,14.555309638438,0.311391073638072));
#42045=CARTESIAN_POINT('Ctrl Pts',(-4.18538433378736,14.5523933457842,0.182262827807668));
#42046=CARTESIAN_POINT('Ctrl Pts',(-4.18922853025337,14.5512835680019,0.0525595133522669));
#42047=CARTESIAN_POINT('Ctrl Pts',(-4.18670294427272,14.5520101946411,-0.0772214321944475));
#42048=CARTESIAN_POINT('Ctrl Pts',(-4.18498039512374,14.5525057826387,-0.165737150534356));
#42049=CARTESIAN_POINT('Ctrl Pts',(-4.1802944723506,14.5538546098955,-0.254288981130209));
#42050=CARTESIAN_POINT('Ctrl Pts',(-4.17262628304436,14.5560527668241,-0.342719102199544));
#42051=CARTESIAN_POINT('Ctrl Pts',(-4.16106584445129,14.5593666727772,-0.476034927301542));
#42052=CARTESIAN_POINT('Ctrl Pts',(-4.14279588034764,14.5645937486684,-0.608312350205319));
#42053=CARTESIAN_POINT('Ctrl Pts',(-4.11795181407459,14.5716147048116,-0.739057191236983));
#42054=CARTESIAN_POINT('Ctrl Pts',(-4.09589395251526,14.5778482769217,-0.855139299993905));
#42055=CARTESIAN_POINT('Ctrl Pts',(-4.06865355383155,14.5854950604866,-0.970013302477714));
#42056=CARTESIAN_POINT('Ctrl Pts',(-4.03631672677125,14.5944383081264,-1.08333333333353));
#42057=CARTESIAN_POINT('',(-3.97254599103887,13.6850786752975,1.08333333333333));
#42058=CARTESIAN_POINT('Ctrl Pts',(-3.97254599103889,13.6850786752975,1.08333333333333));
#42059=CARTESIAN_POINT('Ctrl Pts',(-4.03718797255354,13.8614637488071,1.08333333333333));
#42060=CARTESIAN_POINT('Ctrl Pts',(-4.07292947680577,14.0697175866198,1.08333333333333));
#42061=CARTESIAN_POINT('Ctrl Pts',(-4.07292947680577,14.3589686276554,1.08333333333333));
#42062=CARTESIAN_POINT('Ctrl Pts',(-4.06126656486658,14.4783519618466,1.08333333333333));
#42063=CARTESIAN_POINT('Ctrl Pts',(-4.03631672677098,14.5944383081279,1.08333333333333));
#42064=CARTESIAN_POINT('Ctrl Pts',(-3.97254599103885,13.6850786752975,-1.08333333333333));
#42065=CARTESIAN_POINT('Ctrl Pts',(-4.0055902844374,13.6754864779574,-0.949270311030653));
#42066=CARTESIAN_POINT('Ctrl Pts',(-4.03241557892495,13.6675742096383,-0.813521288368336));
#42067=CARTESIAN_POINT('Ctrl Pts',(-4.05298135839275,13.6614729113855,-0.67660705210156));
#42068=CARTESIAN_POINT('Ctrl Pts',(-4.07056281760631,13.6562569784544,-0.559560573778188));
#42069=CARTESIAN_POINT('Ctrl Pts',(-4.08356944187665,13.6523638057542,-0.441662516279225));
#42070=CARTESIAN_POINT('Ctrl Pts',(-4.09196781162929,13.6498461320482,-0.32323825833471));
#42071=CARTESIAN_POINT('Ctrl Pts',(-4.10167217606822,13.6469369456345,-0.186398348762652));
#42072=CARTESIAN_POINT('Ctrl Pts',(-4.10519527746315,13.6458740742379,-0.0492519096262281));
#42073=CARTESIAN_POINT('Ctrl Pts',(-4.1025698088094,13.6466633637621,0.0876758270660229));
#42074=CARTESIAN_POINT('Ctrl Pts',(-4.09993672885708,13.6474549414561,0.225000520654293));
#42075=CARTESIAN_POINT('Ctrl Pts',(-4.0911193595297,13.6501094100325,0.362105241912746));
#42076=CARTESIAN_POINT('Ctrl Pts',(-4.07613560843688,13.6545823261509,0.498460177595596));
#42077=CARTESIAN_POINT('Ctrl Pts',(-4.06108721528303,13.659074539074,0.635403368116582));
#42078=CARTESIAN_POINT('Ctrl Pts',(-4.03981905948952,13.6654009235528,0.771590289741077));
#42079=CARTESIAN_POINT('Ctrl Pts',(-4.01233468870309,13.673465922941,0.906484242526326));
#42080=CARTESIAN_POINT('Ctrl Pts',(-4.00026996096645,13.6770061903378,0.965698216399675));
#42081=CARTESIAN_POINT('Ctrl Pts',(-3.98700723595603,13.6808808214243,1.02466304565388));
#42082=CARTESIAN_POINT('Ctrl Pts',(-3.97254599103885,13.6850786752975,1.08333333333333));
#42083=CARTESIAN_POINT('',(4.0363167267713,14.5944383081264,-1.08333333333333));
#42084=CARTESIAN_POINT('',(3.97254599103947,13.6850786752973,-1.08333333333333));
#42085=CARTESIAN_POINT('Ctrl Pts',(4.0363167267713,14.5944383081264,-1.08333333333333));
#42086=CARTESIAN_POINT('Ctrl Pts',(4.06125577389196,14.4784021699801,-1.08333333333333));
#42087=CARTESIAN_POINT('Ctrl Pts',(4.07292947680577,14.3589061390379,-1.08333333333333));
#42088=CARTESIAN_POINT('Ctrl Pts',(4.07292947680577,14.0696859538838,-1.08333333333333));
#42089=CARTESIAN_POINT('Ctrl Pts',(4.03699073486477,13.8609255570095,-1.08333333333333));
#42090=CARTESIAN_POINT('Ctrl Pts',(3.97254599103889,13.6850786752975,-1.08333333333333));
#42091=CARTESIAN_POINT('',(3.972545991042,13.685078675306,1.08333333333333));
#42092=CARTESIAN_POINT('Ctrl Pts',(3.97254599103891,13.6850786752974,1.08333333333318));
#42093=CARTESIAN_POINT('Ctrl Pts',(4.00550358468898,13.6755116454224,0.949622058007565));
#42094=CARTESIAN_POINT('Ctrl Pts',(4.03223833992508,13.667626413385,0.814376693553222));
#42095=CARTESIAN_POINT('Ctrl Pts',(4.05275116551691,13.6615412011384,0.678132403728152));
#42096=CARTESIAN_POINT('Ctrl Pts',(4.07316650047532,13.6554849098804,0.542535637670838));
#42097=CARTESIAN_POINT('Ctrl Pts',(4.0874189867075,13.6512115628239,0.40594941879892));
#42098=CARTESIAN_POINT('Ctrl Pts',(4.09549564973878,13.6487880554638,0.268901316711817));
#42099=CARTESIAN_POINT('Ctrl Pts',(4.10076932144717,13.6472056219574,0.179415511018788));
#42100=CARTESIAN_POINT('Ctrl Pts',(4.10340966592831,13.6464108509735,0.0897327832366672));
#42101=CARTESIAN_POINT('Ctrl Pts',(4.10340966592831,13.6464108509735,-4.66293670342566E-15));
#42102=CARTESIAN_POINT('Ctrl Pts',(4.10340966592831,13.6464108509735,-0.137573936980382));
#42103=CARTESIAN_POINT('Ctrl Pts',(4.09720533291532,13.6482810316174,-0.274951212619736));
#42104=CARTESIAN_POINT('Ctrl Pts',(4.08483748845152,13.6519816397819,-0.41161240621476));
#42105=CARTESIAN_POINT('Ctrl Pts',(4.07237395114171,13.6557108803995,-0.549330978772818));
#42106=CARTESIAN_POINT('Ctrl Pts',(4.05365110225785,13.6612989721827,-0.686322345436846));
#42107=CARTESIAN_POINT('Ctrl Pts',(4.02869583028489,13.6686542829587,-0.822054935347102));
#42108=CARTESIAN_POINT('Ctrl Pts',(4.01257796374822,13.6734048590114,-0.909720570537157));
#42109=CARTESIAN_POINT('Ctrl Pts',(3.99385994844905,13.6788915953345,-0.996861109122728));
#42110=CARTESIAN_POINT('Ctrl Pts',(3.97254599103891,13.6850786752974,-1.08333333333318));
#42111=CARTESIAN_POINT('',(4.0363167267713,14.5944383081264,1.08333333333333));
#42112=CARTESIAN_POINT('Ctrl Pts',(4.0363167267713,14.5944383081264,1.08333333333333));
#42113=CARTESIAN_POINT('Ctrl Pts',(4.06125577389196,14.4784021699801,1.08333333333333));
#42114=CARTESIAN_POINT('Ctrl Pts',(4.07292947680577,14.3589061390379,1.08333333333333));
#42115=CARTESIAN_POINT('Ctrl Pts',(4.07292947680577,14.0696859538867,1.08333333333333));
#42116=CARTESIAN_POINT('Ctrl Pts',(4.03699073486612,13.8609255570161,1.08333333333333));
#42117=CARTESIAN_POINT('Ctrl Pts',(3.97254599104201,13.685078675306,1.08333333333333));
#42118=CARTESIAN_POINT('Ctrl Pts',(4.0363167267713,14.5944383081264,-1.08333333333333));
#42119=CARTESIAN_POINT('Ctrl Pts',(4.07267660468553,14.5843824238018,-0.955915065626592));
#42120=CARTESIAN_POINT('Ctrl Pts',(4.10254364280131,14.5759803979714,-0.826701571450557));
#42121=CARTESIAN_POINT('Ctrl Pts',(4.12584816889326,14.5693808768856,-0.696211209492171));
#42122=CARTESIAN_POINT('Ctrl Pts',(4.14878536602558,14.5628853783063,-0.567777653525462));
#42123=CARTESIAN_POINT('Ctrl Pts',(4.16536539316191,14.5581360328796,-0.438107164856169));
#42124=CARTESIAN_POINT('Ctrl Pts',(4.17550906341001,14.5552260824043,-0.307693975181436));
#42125=CARTESIAN_POINT('Ctrl Pts',(4.18345734283739,14.55294593144,-0.205506064179161));
#42126=CARTESIAN_POINT('Ctrl Pts',(4.18745357006455,14.5517942140162,-0.102862147740973));
#42127=CARTESIAN_POINT('Ctrl Pts',(4.18745357006455,14.5517942140162,4.44089209850063E-16));
#42128=CARTESIAN_POINT('Ctrl Pts',(4.18745357006455,14.5517942140162,0.13066680730557));
#42129=CARTESIAN_POINT('Ctrl Pts',(4.18100368362964,14.5536548201376,0.261069786498731));
#42130=CARTESIAN_POINT('Ctrl Pts',(4.16817103415993,14.5573291670729,0.390710450871123));
#42131=CARTESIAN_POINT('Ctrl Pts',(4.15518429935153,14.561047632956,0.521907748246283));
#42132=CARTESIAN_POINT('Ctrl Pts',(4.13566054561854,14.5666236366129,0.652324314224272));
#42133=CARTESIAN_POINT('Ctrl Pts',(4.10965488440249,14.5739568744946,0.781443489202978));
#42134=CARTESIAN_POINT('Ctrl Pts',(4.08920880779353,14.5797223861759,0.882959098491578));
#42135=CARTESIAN_POINT('Ctrl Pts',(4.06475571708163,14.586573067282,0.983672743459539));
#42136=CARTESIAN_POINT('Ctrl Pts',(4.0363167267713,14.5944383081264,1.08333333333333));
#42137=CARTESIAN_POINT('Origin',(0.,0.,-1.08333333333333));
#42138=CARTESIAN_POINT('Origin',(0.,0.,1.08333333333333));
#42139=CARTESIAN_POINT('Origin',(0.,0.,-1.08333333333333));
#42140=CARTESIAN_POINT('Origin',(0.,0.,-1.08333333333333));
#42141=CARTESIAN_POINT('Origin',(0.,0.,-1.08333333333333));
#42142=CARTESIAN_POINT('Origin',(0.,0.,1.08333333333333));
#42143=CARTESIAN_POINT('Origin',(0.,0.,-1.08333333333333));
#42144=CARTESIAN_POINT('Origin',(0.,0.,1.08333333333333));
#42145=CARTESIAN_POINT('Origin',(0.,15.1423076923077,-3.45272288248773));
#42146=CARTESIAN_POINT('Origin',(0.,13.3576923076923,-3.45272288248773));
#42147=CARTESIAN_POINT('Origin',(0.,0.,-1.08333333333333));
#42148=CARTESIAN_POINT('Origin',(0.,0.,-1.08333333333333));
#42149=CARTESIAN_POINT('Origin',(0.,0.,-1.08333333333333));
#42150=CARTESIAN_POINT('Origin',(0.,0.,1.08333333333333));
#42151=CARTESIAN_POINT('Origin',(0.,0.,1.08333333333333));
#42152=CARTESIAN_POINT('Origin',(0.,0.,1.08333333333333));
#42153=CARTESIAN_POINT('Origin',(0.,0.,-1.08333333333333));
#42154=CARTESIAN_POINT('Origin',(0.,0.,-1.08333333333333));
#42155=CARTESIAN_POINT('Origin',(10.4434643792748,8.32838493021314,-3.45272288248773));
#42156=CARTESIAN_POINT('Origin',(11.8387328710639,9.44107442276104,-3.45272288248773));
#42157=CARTESIAN_POINT('Origin',(-1.55588456152528E-16,7.49274514625042E-17,
1.08333333333333));
#42158=CARTESIAN_POINT('Origin',(-1.55588456152528E-16,7.49274514625042E-17,
1.08333333333333));
#42159=CARTESIAN_POINT('Origin',(-1.55588456152528E-16,7.49274514625042E-17,
1.08333333333333));
#42160=CARTESIAN_POINT('Origin',(1.55588456152528E-16,-7.49274514625042E-17,
-1.08333333333333));
#42161=CARTESIAN_POINT('Origin',(1.55588456152528E-16,-7.49274514625042E-17,
-1.08333333333333));
#42162=CARTESIAN_POINT('Origin',(1.55588456152528E-16,-7.49274514625042E-17,
-1.08333333333333));
#42163=CARTESIAN_POINT('Origin',(1.55588456152528E-16,-7.49274514625042E-17,
-1.08333333333333));
#42164=CARTESIAN_POINT('Origin',(1.55588456152528E-16,-7.49274514625042E-17,
-1.08333333333333));
#42165=CARTESIAN_POINT('Origin',(1.94015631396094E-16,-2.43287906657286E-16,
-1.08333333333333));
#42166=CARTESIAN_POINT('Origin',(-1.94015631396094E-16,2.43287906657286E-16,
1.08333333333333));
#42167=CARTESIAN_POINT('Origin',(1.94015631396094E-16,-2.43287906657286E-16,
-1.08333333333333));
#42168=CARTESIAN_POINT('Origin',(1.94015631396094E-16,-2.43287906657286E-16,
-1.08333333333333));
#42169=CARTESIAN_POINT('Origin',(1.94015631396094E-16,-2.43287906657286E-16,
-1.08333333333333));
#42170=CARTESIAN_POINT('Origin',(-1.94015631396094E-16,2.43287906657286E-16,
1.08333333333333));
#42171=CARTESIAN_POINT('Origin',(-1.94015631396094E-16,2.43287906657286E-16,
1.08333333333333));
#42172=CARTESIAN_POINT('Origin',(1.94015631396094E-16,-2.43287906657286E-16,
-1.08333333333333));
#42173=CARTESIAN_POINT('Origin',(13.0227870731057,-2.97236616780865,-3.45272288248773));
#42174=CARTESIAN_POINT('Origin',(14.7626584240763,-3.36948044994605,-3.45272288248773));
#42175=CARTESIAN_POINT('Origin',(-1.94015631396094E-16,2.43287906657286E-16,
1.08333333333333));
#42176=CARTESIAN_POINT('Origin',(-1.94015631396094E-16,2.43287906657286E-16,
1.08333333333333));
#42177=CARTESIAN_POINT('Origin',(-1.94015631396094E-16,2.43287906657286E-16,
1.08333333333333));
#42178=CARTESIAN_POINT('Origin',(1.94015631396094E-16,-2.43287906657286E-16,
-1.08333333333333));
#42179=CARTESIAN_POINT('Origin',(1.94015631396094E-16,-2.43287906657286E-16,
-1.08333333333333));
#42180=CARTESIAN_POINT('Origin',(1.94015631396094E-16,-2.43287906657286E-16,
-1.08333333333333));
#42181=CARTESIAN_POINT('Origin',(1.94015631396094E-16,-2.43287906657286E-16,
-1.08333333333333));
#42182=CARTESIAN_POINT('Origin',(1.94015631396094E-16,-2.43287906657286E-16,
-1.08333333333333));
#42183=CARTESIAN_POINT('Origin',(8.63450790007668E-17,-3.78302508895262E-16,
-1.08333333333333));
#42184=CARTESIAN_POINT('Origin',(-8.63450790007668E-17,3.78302508895262E-16,
1.08333333333333));
#42185=CARTESIAN_POINT('Origin',(8.63450790007668E-17,-3.78302508895262E-16,
-1.08333333333333));
#42186=CARTESIAN_POINT('Origin',(8.63450790007668E-17,-3.78302508895262E-16,
-1.08333333333333));
#42187=CARTESIAN_POINT('Origin',(8.63450790007668E-17,-3.78302508895262E-16,
-1.08333333333333));
#42188=CARTESIAN_POINT('Origin',(-8.63450790007668E-17,3.78302508895262E-16,
1.08333333333333));
#42189=CARTESIAN_POINT('Origin',(-8.63450790007668E-17,3.78302508895262E-16,
1.08333333333333));
#42190=CARTESIAN_POINT('Origin',(8.63450790007668E-17,-3.78302508895262E-16,
-1.08333333333333));
#42191=CARTESIAN_POINT('Origin',(5.79568548444348,-12.0348649162504,-3.45272288248773));
#42192=CARTESIAN_POINT('Origin',(6.57000108040713,-13.6427478189685,-3.45272288248772));
#42193=CARTESIAN_POINT('Origin',(-8.63450790007668E-17,3.78302508895262E-16,
1.08333333333333));
#42194=CARTESIAN_POINT('Origin',(-8.63450790007668E-17,3.78302508895262E-16,
1.08333333333333));
#42195=CARTESIAN_POINT('Origin',(-8.63450790007668E-17,3.78302508895262E-16,
1.08333333333333));
#42196=CARTESIAN_POINT('Origin',(8.63450790007668E-17,-3.78302508895262E-16,
-1.08333333333333));
#42197=CARTESIAN_POINT('Origin',(8.63450790007668E-17,-3.78302508895262E-16,
-1.08333333333333));
#42198=CARTESIAN_POINT('Origin',(8.63450790007668E-17,-3.78302508895262E-16,
-1.08333333333333));
#42199=CARTESIAN_POINT('Origin',(8.63450790007668E-17,-3.78302508895262E-16,
-1.08333333333333));
#42200=CARTESIAN_POINT('Origin',(8.63450790007668E-17,-3.78302508895262E-16,
-1.08333333333333));
#42201=CARTESIAN_POINT('Origin',(-8.63450790007644E-17,-3.78302508895264E-16,
-1.08333333333333));
#42202=CARTESIAN_POINT('Origin',(8.63450790007644E-17,3.78302508895264E-16,
1.08333333333333));
#42203=CARTESIAN_POINT('Origin',(-8.63450790007644E-17,-3.78302508895264E-16,
-1.08333333333333));
#42204=CARTESIAN_POINT('Origin',(-8.63450790007644E-17,-3.78302508895264E-16,
-1.08333333333333));
#42205=CARTESIAN_POINT('Origin',(-8.63450790007644E-17,-3.78302508895264E-16,
-1.08333333333333));
#42206=CARTESIAN_POINT('Origin',(8.63450790007644E-17,3.78302508895264E-16,
1.08333333333333));
#42207=CARTESIAN_POINT('Origin',(8.63450790007644E-17,3.78302508895264E-16,
1.08333333333333));
#42208=CARTESIAN_POINT('Origin',(-8.63450790007644E-17,-3.78302508895264E-16,
-1.08333333333333));
#42209=CARTESIAN_POINT('Origin',(-5.79568548444331,-12.0348649162504,-3.45272288248773));
#42210=CARTESIAN_POINT('Origin',(-6.57000108040694,-13.6427478189686,-3.45272288248772));
#42211=CARTESIAN_POINT('Origin',(8.63450790007644E-17,3.78302508895264E-16,
1.08333333333333));
#42212=CARTESIAN_POINT('Origin',(8.63450790007644E-17,3.78302508895264E-16,
1.08333333333333));
#42213=CARTESIAN_POINT('Origin',(8.63450790007644E-17,3.78302508895264E-16,
1.08333333333333));
#42214=CARTESIAN_POINT('Origin',(-8.63450790007644E-17,-3.78302508895264E-16,
-1.08333333333333));
#42215=CARTESIAN_POINT('Origin',(-8.63450790007644E-17,-3.78302508895264E-16,
-1.08333333333333));
#42216=CARTESIAN_POINT('Origin',(-8.63450790007644E-17,-3.78302508895264E-16,
-1.08333333333333));
#42217=CARTESIAN_POINT('Origin',(-8.63450790007644E-17,-3.78302508895264E-16,
-1.08333333333333));
#42218=CARTESIAN_POINT('Origin',(-8.63450790007644E-17,-3.78302508895264E-16,
-1.08333333333333));
#42219=CARTESIAN_POINT('Origin',(-1.94015631396093E-16,-2.43287906657289E-16,
-1.08333333333333));
#42220=CARTESIAN_POINT('Origin',(1.94015631396093E-16,2.43287906657289E-16,
1.08333333333333));
#42221=CARTESIAN_POINT('Origin',(-1.94015631396093E-16,-2.43287906657289E-16,
-1.08333333333333));
#42222=CARTESIAN_POINT('Origin',(-1.94015631396093E-16,-2.43287906657289E-16,
-1.08333333333333));
#42223=CARTESIAN_POINT('Origin',(-1.94015631396093E-16,-2.43287906657289E-16,
-1.08333333333333));
#42224=CARTESIAN_POINT('Origin',(1.94015631396093E-16,2.43287906657289E-16,
1.08333333333333));
#42225=CARTESIAN_POINT('Origin',(1.94015631396093E-16,2.43287906657289E-16,
1.08333333333333));
#42226=CARTESIAN_POINT('Origin',(-1.94015631396093E-16,-2.43287906657289E-16,
-1.08333333333333));
#42227=CARTESIAN_POINT('Origin',(-13.0227870731057,-2.97236616780882,-3.45272288248773));
#42228=CARTESIAN_POINT('Origin',(-14.7626584240763,-3.36948044994625,-3.45272288248773));
#42229=CARTESIAN_POINT('Origin',(1.94015631396093E-16,2.43287906657289E-16,
1.08333333333333));
#42230=CARTESIAN_POINT('Origin',(1.94015631396093E-16,2.43287906657289E-16,
1.08333333333333));
#42231=CARTESIAN_POINT('Origin',(1.94015631396093E-16,2.43287906657289E-16,
1.08333333333333));
#42232=CARTESIAN_POINT('Origin',(-1.94015631396093E-16,-2.43287906657289E-16,
-1.08333333333333));
#42233=CARTESIAN_POINT('Origin',(-1.94015631396093E-16,-2.43287906657289E-16,
-1.08333333333333));
#42234=CARTESIAN_POINT('Origin',(-1.94015631396093E-16,-2.43287906657289E-16,
-1.08333333333333));
#42235=CARTESIAN_POINT('Origin',(-1.94015631396093E-16,-2.43287906657289E-16,
-1.08333333333333));
#42236=CARTESIAN_POINT('Origin',(-1.94015631396093E-16,-2.43287906657289E-16,
-1.08333333333333));
#42237=CARTESIAN_POINT('Origin',(-1.55588456152529E-16,-7.49274514625064E-17,
-1.08333333333333));
#42238=CARTESIAN_POINT('Origin',(1.55588456152529E-16,7.49274514625064E-17,
1.08333333333333));
#42239=CARTESIAN_POINT('Origin',(-1.55588456152529E-16,-7.49274514625064E-17,
-1.08333333333333));
#42240=CARTESIAN_POINT('Origin',(-1.55588456152529E-16,-7.49274514625064E-17,
-1.08333333333333));
#42241=CARTESIAN_POINT('Origin',(-1.55588456152529E-16,-7.49274514625064E-17,
-1.08333333333333));
#42242=CARTESIAN_POINT('Origin',(1.55588456152529E-16,7.49274514625064E-17,
1.08333333333333));
#42243=CARTESIAN_POINT('Origin',(1.55588456152529E-16,7.49274514625064E-17,
1.08333333333333));
#42244=CARTESIAN_POINT('Origin',(-1.55588456152529E-16,-7.49274514625064E-17,
-1.08333333333333));
#42245=CARTESIAN_POINT('Origin',(-10.4434643792749,8.32838493021299,-3.45272288248773));
#42246=CARTESIAN_POINT('Origin',(-11.838732871064,9.44107442276088,-3.45272288248773));
#42247=CARTESIAN_POINT('Origin',(1.55588456152529E-16,7.49274514625064E-17,
1.08333333333333));
#42248=CARTESIAN_POINT('Origin',(1.55588456152529E-16,7.49274514625064E-17,
1.08333333333333));
#42249=CARTESIAN_POINT('Origin',(1.55588456152529E-16,7.49274514625064E-17,
1.08333333333333));
#42250=CARTESIAN_POINT('Origin',(-1.55588456152529E-16,-7.49274514625064E-17,
-1.08333333333333));
#42251=CARTESIAN_POINT('Origin',(-1.55588456152529E-16,-7.49274514625064E-17,
-1.08333333333333));
#42252=CARTESIAN_POINT('Origin',(-1.55588456152529E-16,-7.49274514625064E-17,
-1.08333333333333));
#42253=CARTESIAN_POINT('Origin',(-1.55588456152529E-16,-7.49274514625064E-17,
-1.08333333333333));
#42254=CARTESIAN_POINT('Origin',(-1.55588456152529E-16,-7.49274514625064E-17,
-1.08333333333333));
#42255=CARTESIAN_POINT('Origin',(0.,0.,-1.08333333333333));
#42256=CARTESIAN_POINT('Origin',(0.,0.,-1.08333333333333));
#42257=CARTESIAN_POINT('Origin',(0.,0.,-1.08333333333333));
#42258=CARTESIAN_POINT('Origin',(0.,0.,1.08333333333333));
#42259=CARTESIAN_POINT('Origin',(0.,0.,1.08333333333333));
#42260=CARTESIAN_POINT('Origin',(0.,0.,1.08333333333333));
#42261=CARTESIAN_POINT('Origin',(0.,0.,-1.08333333333333));
#42262=CARTESIAN_POINT('Origin',(0.,0.,-1.08333333333333));
#43767=UNCERTAINTY_MEASURE_WITH_UNIT(LENGTH_MEASURE(0.01),#43782,
'DISTANCE_ACCURACY_VALUE',
'Maximum model space distance between geometric entities at asserted c
onnectivities');
#43771=UNCERTAINTY_MEASURE_WITH_UNIT(LENGTH_MEASURE(0.01),#43782,
'DISTANCE_ACCURACY_VALUE',
'Maximum model space distance between geometric entities at asserted c
onnectivities');
#43777=(
GEOMETRIC_REPRESENTATION_CONTEXT(3)
GLOBAL_UNCERTAINTY_ASSIGNED_CONTEXT((#43767))
GLOBAL_UNIT_ASSIGNED_CONTEXT((#43782,#43784,#43785))
REPRESENTATION_CONTEXT('','3D')
);
#43781=(
GEOMETRIC_REPRESENTATION_CONTEXT(3)
GLOBAL_UNCERTAINTY_ASSIGNED_CONTEXT((#43771))
GLOBAL_UNIT_ASSIGNED_CONTEXT((#43782,#43784,#43785))
REPRESENTATION_CONTEXT('','3D')
);
#43782=(
LENGTH_UNIT()
NAMED_UNIT(*)
SI_UNIT(.MILLI.,.METRE.)
);
#43784=(
NAMED_UNIT(*)
PLANE_ANGLE_UNIT()
SI_UNIT($,.RADIAN.)
);
#43785=(
NAMED_UNIT(*)
SI_UNIT($,.STERADIAN.)
SOLID_ANGLE_UNIT()
);
#43791=SHAPE_DEFINITION_REPRESENTATION(#43800,#43817);
#43800=PRODUCT_DEFINITION_SHAPE('',$,#43827);
#43817=SHAPE_REPRESENTATION('',(#14253),#43777);
#43821=PRODUCT_DEFINITION_CONTEXT('part definition',#43850,'design');
#43827=PRODUCT_DEFINITION('5972K117_Steel Ball Bearing_2','Bearing_03',
#43836,#43821);
#43836=PRODUCT_DEFINITION_FORMATION('',$,#43857);
#43850=APPLICATION_CONTEXT(
'Core Data for Automotive Mechanical Design Process');
#43851=PRODUCT_CONTEXT('part definition',#43850,'mechanical');
#43857=PRODUCT('5972K117_Steel Ball Bearing_2','Bearing_03',$,(#43851));
#43863=PRESENTATION_STYLE_ASSIGNMENT((#43866));
#43866=SURFACE_STYLE_USAGE(.BOTH.,#43869);
#43869=SURFACE_SIDE_STYLE('',(#43872));
#43872=SURFACE_STYLE_FILL_AREA(#43875);
#43875=FILL_AREA_STYLE('Opaque(160,160,160)',(#43878));
#43878=FILL_AREA_STYLE_COLOUR('Opaque(160,160,160)',#43881);
#43881=COLOUR_RGB('Opaque(160,160,160)', 0.31764706, 0.68627451, 0.89019608);
ENDSEC;
END-ISO-10303-21;
